ISO-10303-21;
HEADER;
/* Generated by software containing ST-Developer
 * from STEP Tools, Inc. (www.steptools.com) 
 */

FILE_DESCRIPTION(
/* description */ (''),
/* implementation_level */ '2;1');

FILE_NAME(
/* name */ 'Bracket_01 (1).step',
/* time_stamp */ '2026-10-22T15:07:41+06:00',
/* author */ (''),
/* organization */ (''),
/* preprocessor_version */ 'ST-DEVELOPER v20.2',
/* originating_system */ 'Autodesk Translation Framework v15.15.0.0',
/* authorisation */ '');

FILE_SCHEMA (('AUTOMOTIVE_DESIGN { 1 0 10303 214 3 1 1 }'));
ENDSEC;

DATA;
#10=MECHANICAL_DESIGN_GEOMETRIC_PRESENTATION_REPRESENTATION('',(#2884),#19220);
#73=SHAPE_REPRESENTATION_RELATIONSHIP('SRR','None',#19276,#87);
#87=ADVANCED_BREP_SHAPE_REPRESENTATION('',(#101),#19212);
#101=MANIFOLD_SOLID_BREP('Bracket_01',#11320);
#515=FACE_BOUND('',#4213,.T.);
#516=FACE_BOUND('',#4214,.T.);
#517=FACE_BOUND('',#4215,.T.);
#518=FACE_BOUND('',#4216,.T.);
#519=FACE_BOUND('',#4217,.T.);
#520=FACE_BOUND('',#4218,.T.);
#521=FACE_BOUND('',#4219,.T.);
#522=FACE_BOUND('',#4220,.T.);
#523=FACE_BOUND('',#4221,.T.);
#524=FACE_BOUND('',#4222,.T.);
#525=FACE_BOUND('',#4223,.T.);
#526=FACE_BOUND('',#4226,.T.);
#527=FACE_BOUND('',#4227,.T.);
#528=FACE_BOUND('',#4228,.T.);
#529=FACE_BOUND('',#4229,.T.);
#530=FACE_BOUND('',#4230,.T.);
#531=FACE_BOUND('',#4231,.T.);
#532=FACE_BOUND('',#4232,.T.);
#533=FACE_BOUND('',#4233,.T.);
#534=FACE_BOUND('',#4234,.T.);
#535=FACE_BOUND('',#4235,.T.);
#536=FACE_BOUND('',#4236,.T.);
#537=FACE_BOUND('',#4254,.T.);
#538=FACE_BOUND('',#4255,.T.);
#539=FACE_BOUND('',#4256,.T.);
#540=FACE_BOUND('',#4257,.T.);
#541=FACE_BOUND('',#4258,.T.);
#542=FACE_BOUND('',#4259,.T.);
#543=FACE_BOUND('',#4260,.T.);
#544=FACE_BOUND('',#4261,.T.);
#545=FACE_BOUND('',#4262,.T.);
#546=FACE_BOUND('',#4263,.T.);
#547=FACE_BOUND('',#4264,.T.);
#548=FACE_BOUND('',#4282,.T.);
#549=FACE_BOUND('',#4283,.T.);
#550=FACE_BOUND('',#4284,.T.);
#551=FACE_BOUND('',#4285,.T.);
#552=FACE_BOUND('',#4286,.T.);
#553=FACE_BOUND('',#4287,.T.);
#554=FACE_BOUND('',#4288,.T.);
#555=FACE_BOUND('',#4289,.T.);
#556=FACE_BOUND('',#4290,.T.);
#557=FACE_BOUND('',#4291,.T.);
#558=FACE_BOUND('',#4292,.T.);
#559=FACE_BOUND('',#4294,.T.);
#560=FACE_BOUND('',#4295,.T.);
#561=FACE_BOUND('',#4296,.T.);
#562=FACE_BOUND('',#4298,.T.);
#563=FACE_BOUND('',#4301,.T.);
#564=FACE_BOUND('',#4302,.T.);
#732=PLANE('',#12387);
#733=PLANE('',#12402);
#734=PLANE('',#12425);
#735=PLANE('',#12426);
#736=PLANE('',#12427);
#737=PLANE('',#12428);
#738=PLANE('',#12429);
#739=PLANE('',#12430);
#740=PLANE('',#12464);
#741=PLANE('',#12465);
#742=PLANE('',#12466);
#743=PLANE('',#12467);
#744=PLANE('',#12468);
#745=PLANE('',#12469);
#746=PLANE('',#12470);
#747=PLANE('',#12471);
#748=PLANE('',#12472);
#749=PLANE('',#12473);
#750=PLANE('',#12474);
#751=PLANE('',#12475);
#1349=LINE('',#18165,#2204);
#1350=LINE('',#18171,#2205);
#1351=LINE('',#18177,#2206);
#1352=LINE('',#18184,#2207);
#1353=LINE('',#18187,#2208);
#1354=LINE('',#18190,#2209);
#1355=LINE('',#18192,#2210);
#1356=LINE('',#18194,#2211);
#1357=LINE('',#18196,#2212);
#1358=LINE('',#18198,#2213);
#1359=LINE('',#18200,#2214);
#1360=LINE('',#18201,#2215);
#1361=LINE('',#18229,#2216);
#1362=LINE('',#18232,#2217);
#1363=LINE('',#18235,#2218);
#1364=LINE('',#18237,#2219);
#1365=LINE('',#18239,#2220);
#1366=LINE('',#18241,#2221);
#1367=LINE('',#18243,#2222);
#1368=LINE('',#18245,#2223);
#1369=LINE('',#18246,#2224);
#1370=LINE('',#18270,#2225);
#1371=LINE('',#18272,#2226);
#1372=LINE('',#18274,#2227);
#1373=LINE('',#18276,#2228);
#1374=LINE('',#18278,#2229);
#1375=LINE('',#18280,#2230);
#1376=LINE('',#18282,#2231);
#1377=LINE('',#18284,#2232);
#1378=LINE('',#18286,#2233);
#1379=LINE('',#18288,#2234);
#1380=LINE('',#18290,#2235);
#1381=LINE('',#18292,#2236);
#1382=LINE('',#18293,#2237);
#1383=LINE('',#18295,#2238);
#1384=LINE('',#18296,#2239);
#1385=LINE('',#18298,#2240);
#1386=LINE('',#18300,#2241);
#1387=LINE('',#18305,#2242);
#1388=LINE('',#18307,#2243);
#1389=LINE('',#18309,#2244);
#1390=LINE('',#18311,#2245);
#1391=LINE('',#18313,#2246);
#1392=LINE('',#18315,#2247);
#1393=LINE('',#18317,#2248);
#1394=LINE('',#18318,#2249);
#1395=LINE('',#18344,#2250);
#1396=LINE('',#18348,#2251);
#1397=LINE('',#18352,#2252);
#1398=LINE('',#18356,#2253);
#1399=LINE('',#18360,#2254);
#1400=LINE('',#18364,#2255);
#1401=LINE('',#18368,#2256);
#1402=LINE('',#18372,#2257);
#1403=LINE('',#18376,#2258);
#1404=LINE('',#18380,#2259);
#1405=LINE('',#18384,#2260);
#1406=LINE('',#18387,#2261);
#1407=LINE('',#18389,#2262);
#1408=LINE('',#18390,#2263);
#1409=LINE('',#18393,#2264);
#1410=LINE('',#18395,#2265);
#1411=LINE('',#18396,#2266);
#1412=LINE('',#18399,#2267);
#1413=LINE('',#18400,#2268);
#1414=LINE('',#18403,#2269);
#1415=LINE('',#18404,#2270);
#1416=LINE('',#18406,#2271);
#1417=LINE('',#18410,#2272);
#1418=LINE('',#18411,#2273);
#1419=LINE('',#18412,#2274);
#1420=LINE('',#18415,#2275);
#1421=LINE('',#18417,#2276);
#1422=LINE('',#18418,#2277);
#1423=LINE('',#18420,#2278);
#1424=LINE('',#18421,#2279);
#1425=LINE('',#18424,#2280);
#1426=LINE('',#18425,#2281);
#1427=LINE('',#18428,#2282);
#1428=LINE('',#18429,#2283);
#1429=LINE('',#18431,#2284);
#2204=VECTOR('',#15026,1.49999999999999);
#2205=VECTOR('',#15033,2.00000000000003);
#2206=VECTOR('',#15040,2.00000000000003);
#2207=VECTOR('',#15047,10.);
#2208=VECTOR('',#15050,10.);
#2209=VECTOR('',#15053,10.);
#2210=VECTOR('',#15054,10.);
#2211=VECTOR('',#15055,10.);
#2212=VECTOR('',#15056,10.);
#2213=VECTOR('',#15057,10.);
#2214=VECTOR('',#15058,10.);
#2215=VECTOR('',#15059,10.);
#2216=VECTOR('',#15086,4.);
#2217=VECTOR('',#15089,10.);
#2218=VECTOR('',#15092,10.);
#2219=VECTOR('',#15093,10.);
#2220=VECTOR('',#15094,10.);
#2221=VECTOR('',#15095,10.);
#2222=VECTOR('',#15096,10.);
#2223=VECTOR('',#15097,10.);
#2224=VECTOR('',#15098,10.);
#2225=VECTOR('',#15123,1.49999999999999);
#2226=VECTOR('',#15126,1.49999999999999);
#2227=VECTOR('',#15129,1.49999999999999);
#2228=VECTOR('',#15132,1.49999999999999);
#2229=VECTOR('',#15135,1.49999999999999);
#2230=VECTOR('',#15138,1.49999999999999);
#2231=VECTOR('',#15141,1.49999999999999);
#2232=VECTOR('',#15144,1.49999999999999);
#2233=VECTOR('',#15147,1.49999999999999);
#2234=VECTOR('',#15150,1.49999999999999);
#2235=VECTOR('',#15153,1.49999999999999);
#2236=VECTOR('',#15156,10.);
#2237=VECTOR('',#15157,10.);
#2238=VECTOR('',#15160,10.);
#2239=VECTOR('',#15161,10.);
#2240=VECTOR('',#15164,10.);
#2241=VECTOR('',#15167,10.);
#2242=VECTOR('',#15172,10.);
#2243=VECTOR('',#15173,10.);
#2244=VECTOR('',#15174,10.);
#2245=VECTOR('',#15175,10.);
#2246=VECTOR('',#15176,10.);
#2247=VECTOR('',#15177,10.);
#2248=VECTOR('',#15178,10.);
#2249=VECTOR('',#15179,10.);
#2250=VECTOR('',#15206,1.49999999999999);
#2251=VECTOR('',#15211,1.49999999999999);
#2252=VECTOR('',#15216,1.49999999999999);
#2253=VECTOR('',#15221,1.49999999999999);
#2254=VECTOR('',#15226,1.49999999999999);
#2255=VECTOR('',#15231,1.49999999999999);
#2256=VECTOR('',#15236,1.49999999999999);
#2257=VECTOR('',#15241,1.49999999999999);
#2258=VECTOR('',#15246,1.49999999999999);
#2259=VECTOR('',#15251,1.49999999999999);
#2260=VECTOR('',#15256,1.49999999999999);
#2261=VECTOR('',#15259,10.);
#2262=VECTOR('',#15260,10.);
#2263=VECTOR('',#15261,10.);
#2264=VECTOR('',#15264,10.);
#2265=VECTOR('',#15265,10.);
#2266=VECTOR('',#15266,10.);
#2267=VECTOR('',#15269,10.);
#2268=VECTOR('',#15270,10.);
#2269=VECTOR('',#15273,10.);
#2270=VECTOR('',#15274,10.);
#2271=VECTOR('',#15277,10.);
#2272=VECTOR('',#15280,10.);
#2273=VECTOR('',#15281,10.);
#2274=VECTOR('',#15282,10.);
#2275=VECTOR('',#15285,10.);
#2276=VECTOR('',#15286,10.);
#2277=VECTOR('',#15287,10.);
#2278=VECTOR('',#15290,10.);
#2279=VECTOR('',#15291,10.);
#2280=VECTOR('',#15294,10.);
#2281=VECTOR('',#15295,10.);
#2282=VECTOR('',#15298,10.);
#2283=VECTOR('',#15299,10.);
#2284=VECTOR('',#15302,10.);
#2801=CYLINDRICAL_SURFACE('',#12375,1.49999999999999);
#2802=CYLINDRICAL_SURFACE('',#12378,2.00000000000003);
#2803=CYLINDRICAL_SURFACE('',#12381,2.00000000000003);
#2804=CYLINDRICAL_SURFACE('',#12384,2.);
#2805=CYLINDRICAL_SURFACE('',#12399,4.);
#2806=CYLINDRICAL_SURFACE('',#12414,1.49999999999999);
#2807=CYLINDRICAL_SURFACE('',#12415,1.49999999999999);
#2808=CYLINDRICAL_SURFACE('',#12416,1.49999999999999);
#2809=CYLINDRICAL_SURFACE('',#12417,1.49999999999999);
#2810=CYLINDRICAL_SURFACE('',#12418,1.49999999999999);
#2811=CYLINDRICAL_SURFACE('',#12419,1.49999999999999);
#2812=CYLINDRICAL_SURFACE('',#12420,1.49999999999999);
#2813=CYLINDRICAL_SURFACE('',#12421,1.49999999999999);
#2814=CYLINDRICAL_SURFACE('',#12422,1.49999999999999);
#2815=CYLINDRICAL_SURFACE('',#12423,1.49999999999999);
#2816=CYLINDRICAL_SURFACE('',#12424,1.49999999999999);
#2817=CYLINDRICAL_SURFACE('',#12442,1.49999999999999);
#2818=CYLINDRICAL_SURFACE('',#12444,1.49999999999999);
#2819=CYLINDRICAL_SURFACE('',#12446,1.49999999999999);
#2820=CYLINDRICAL_SURFACE('',#12448,1.49999999999999);
#2821=CYLINDRICAL_SURFACE('',#12450,1.49999999999999);
#2822=CYLINDRICAL_SURFACE('',#12452,1.49999999999999);
#2823=CYLINDRICAL_SURFACE('',#12454,1.49999999999999);
#2824=CYLINDRICAL_SURFACE('',#12456,1.49999999999999);
#2825=CYLINDRICAL_SURFACE('',#12458,1.49999999999999);
#2826=CYLINDRICAL_SURFACE('',#12460,1.49999999999999);
#2827=CYLINDRICAL_SURFACE('',#12462,1.49999999999999);
#2884=STYLED_ITEM('',(#19382),#101);
#3256=FACE_OUTER_BOUND('',#4208,.T.);
#3257=FACE_OUTER_BOUND('',#4209,.T.);
#3258=FACE_OUTER_BOUND('',#4210,.T.);
#3259=FACE_OUTER_BOUND('',#4211,.T.);
#3260=FACE_OUTER_BOUND('',#4212,.T.);
#3261=FACE_OUTER_BOUND('',#4224,.T.);
#3262=FACE_OUTER_BOUND('',#4225,.T.);
#3263=FACE_OUTER_BOUND('',#4237,.T.);
#3264=FACE_OUTER_BOUND('',#4238,.T.);
#3265=FACE_OUTER_BOUND('',#4239,.T.);
#3266=FACE_OUTER_BOUND('',#4240,.T.);
#3267=FACE_OUTER_BOUND('',#4241,.T.);
#3268=FACE_OUTER_BOUND('',#4242,.T.);
#3269=FACE_OUTER_BOUND('',#4243,.T.);
#3270=FACE_OUTER_BOUND('',#4244,.T.);
#3271=FACE_OUTER_BOUND('',#4245,.T.);
#3272=FACE_OUTER_BOUND('',#4246,.T.);
#3273=FACE_OUTER_BOUND('',#4247,.T.);
#3274=FACE_OUTER_BOUND('',#4248,.T.);
#3275=FACE_OUTER_BOUND('',#4249,.T.);
#3276=FACE_OUTER_BOUND('',#4250,.T.);
#3277=FACE_OUTER_BOUND('',#4251,.T.);
#3278=FACE_OUTER_BOUND('',#4252,.T.);
#3279=FACE_OUTER_BOUND('',#4253,.T.);
#3280=FACE_OUTER_BOUND('',#4265,.T.);
#3281=FACE_OUTER_BOUND('',#4266,.T.);
#3282=FACE_OUTER_BOUND('',#4267,.T.);
#3283=FACE_OUTER_BOUND('',#4268,.T.);
#3284=FACE_OUTER_BOUND('',#4269,.T.);
#3285=FACE_OUTER_BOUND('',#4270,.T.);
#3286=FACE_OUTER_BOUND('',#4271,.T.);
#3287=FACE_OUTER_BOUND('',#4272,.T.);
#3288=FACE_OUTER_BOUND('',#4273,.T.);
#3289=FACE_OUTER_BOUND('',#4274,.T.);
#3290=FACE_OUTER_BOUND('',#4275,.T.);
#3291=FACE_OUTER_BOUND('',#4276,.T.);
#3292=FACE_OUTER_BOUND('',#4277,.T.);
#3293=FACE_OUTER_BOUND('',#4278,.T.);
#3294=FACE_OUTER_BOUND('',#4279,.T.);
#3295=FACE_OUTER_BOUND('',#4280,.T.);
#3296=FACE_OUTER_BOUND('',#4281,.T.);
#3297=FACE_OUTER_BOUND('',#4293,.T.);
#3298=FACE_OUTER_BOUND('',#4297,.T.);
#3299=FACE_OUTER_BOUND('',#4299,.T.);
#3300=FACE_OUTER_BOUND('',#4300,.T.);
#3301=FACE_OUTER_BOUND('',#4303,.T.);
#3302=FACE_OUTER_BOUND('',#4304,.T.);
#4208=EDGE_LOOP('',(#9772,#9773,#9774,#9775));
#4209=EDGE_LOOP('',(#9776,#9777,#9778,#9779));
#4210=EDGE_LOOP('',(#9780,#9781,#9782,#9783));
#4211=EDGE_LOOP('',(#9784,#9785,#9786,#9787));
#4212=EDGE_LOOP('',(#9788,#9789,#9790,#9791,#9792,#9793,#9794,#9795));
#4213=EDGE_LOOP('',(#9796));
#4214=EDGE_LOOP('',(#9797));
#4215=EDGE_LOOP('',(#9798));
#4216=EDGE_LOOP('',(#9799));
#4217=EDGE_LOOP('',(#9800));
#4218=EDGE_LOOP('',(#9801));
#4219=EDGE_LOOP('',(#9802));
#4220=EDGE_LOOP('',(#9803));
#4221=EDGE_LOOP('',(#9804));
#4222=EDGE_LOOP('',(#9805));
#4223=EDGE_LOOP('',(#9806));
#4224=EDGE_LOOP('',(#9807,#9808,#9809,#9810));
#4225=EDGE_LOOP('',(#9811,#9812,#9813,#9814,#9815,#9816,#9817,#9818));
#4226=EDGE_LOOP('',(#9819));
#4227=EDGE_LOOP('',(#9820));
#4228=EDGE_LOOP('',(#9821));
#4229=EDGE_LOOP('',(#9822));
#4230=EDGE_LOOP('',(#9823));
#4231=EDGE_LOOP('',(#9824));
#4232=EDGE_LOOP('',(#9825));
#4233=EDGE_LOOP('',(#9826));
#4234=EDGE_LOOP('',(#9827));
#4235=EDGE_LOOP('',(#9828));
#4236=EDGE_LOOP('',(#9829));
#4237=EDGE_LOOP('',(#9830,#9831,#9832,#9833));
#4238=EDGE_LOOP('',(#9834,#9835,#9836,#9837));
#4239=EDGE_LOOP('',(#9838,#9839,#9840,#9841));
#4240=EDGE_LOOP('',(#9842,#9843,#9844,#9845));
#4241=EDGE_LOOP('',(#9846,#9847,#9848,#9849));
#4242=EDGE_LOOP('',(#9850,#9851,#9852,#9853));
#4243=EDGE_LOOP('',(#9854,#9855,#9856,#9857));
#4244=EDGE_LOOP('',(#9858,#9859,#9860,#9861));
#4245=EDGE_LOOP('',(#9862,#9863,#9864,#9865));
#4246=EDGE_LOOP('',(#9866,#9867,#9868,#9869));
#4247=EDGE_LOOP('',(#9870,#9871,#9872,#9873));
#4248=EDGE_LOOP('',(#9874,#9875,#9876,#9877));
#4249=EDGE_LOOP('',(#9878,#9879,#9880,#9881));
#4250=EDGE_LOOP('',(#9882,#9883,#9884,#9885));
#4251=EDGE_LOOP('',(#9886,#9887,#9888,#9889));
#4252=EDGE_LOOP('',(#9890,#9891,#9892,#9893));
#4253=EDGE_LOOP('',(#9894,#9895,#9896,#9897,#9898,#9899,#9900,#9901));
#4254=EDGE_LOOP('',(#9902));
#4255=EDGE_LOOP('',(#9903));
#4256=EDGE_LOOP('',(#9904));
#4257=EDGE_LOOP('',(#9905));
#4258=EDGE_LOOP('',(#9906));
#4259=EDGE_LOOP('',(#9907));
#4260=EDGE_LOOP('',(#9908));
#4261=EDGE_LOOP('',(#9909));
#4262=EDGE_LOOP('',(#9910));
#4263=EDGE_LOOP('',(#9911));
#4264=EDGE_LOOP('',(#9912));
#4265=EDGE_LOOP('',(#9913,#9914,#9915,#9916));
#4266=EDGE_LOOP('',(#9917,#9918,#9919,#9920));
#4267=EDGE_LOOP('',(#9921,#9922,#9923,#9924));
#4268=EDGE_LOOP('',(#9925,#9926,#9927,#9928));
#4269=EDGE_LOOP('',(#9929,#9930,#9931,#9932));
#4270=EDGE_LOOP('',(#9933,#9934,#9935,#9936));
#4271=EDGE_LOOP('',(#9937,#9938,#9939,#9940));
#4272=EDGE_LOOP('',(#9941,#9942,#9943,#9944));
#4273=EDGE_LOOP('',(#9945,#9946,#9947,#9948));
#4274=EDGE_LOOP('',(#9949,#9950,#9951,#9952));
#4275=EDGE_LOOP('',(#9953,#9954,#9955,#9956));
#4276=EDGE_LOOP('',(#9957,#9958,#9959,#9960));
#4277=EDGE_LOOP('',(#9961,#9962,#9963,#9964));
#4278=EDGE_LOOP('',(#9965,#9966,#9967,#9968));
#4279=EDGE_LOOP('',(#9969,#9970,#9971,#9972));
#4280=EDGE_LOOP('',(#9973,#9974,#9975,#9976));
#4281=EDGE_LOOP('',(#9977,#9978,#9979,#9980,#9981,#9982,#9983,#9984));
#4282=EDGE_LOOP('',(#9985));
#4283=EDGE_LOOP('',(#9986));
#4284=EDGE_LOOP('',(#9987));
#4285=EDGE_LOOP('',(#9988));
#4286=EDGE_LOOP('',(#9989));
#4287=EDGE_LOOP('',(#9990));
#4288=EDGE_LOOP('',(#9991));
#4289=EDGE_LOOP('',(#9992));
#4290=EDGE_LOOP('',(#9993));
#4291=EDGE_LOOP('',(#9994));
#4292=EDGE_LOOP('',(#9995));
#4293=EDGE_LOOP('',(#9996,#9997,#9998,#9999));
#4294=EDGE_LOOP('',(#10000));
#4295=EDGE_LOOP('',(#10001));
#4296=EDGE_LOOP('',(#10002));
#4297=EDGE_LOOP('',(#10003,#10004,#10005,#10006));
#4298=EDGE_LOOP('',(#10007));
#4299=EDGE_LOOP('',(#10008,#10009,#10010,#10011,#10012,#10013,#10014,#10015,
#10016,#10017,#10018,#10019));
#4300=EDGE_LOOP('',(#10020,#10021,#10022,#10023));
#4301=EDGE_LOOP('',(#10024));
#4302=EDGE_LOOP('',(#10025));
#4303=EDGE_LOOP('',(#10026,#10027,#10028,#10029,#10030,#10031,#10032,#10033,
#10034,#10035,#10036,#10037));
#4304=EDGE_LOOP('',(#10038,#10039,#10040,#10041));
#5021=CIRCLE('',#12376,1.49999999999999);
#5022=CIRCLE('',#12377,1.49999999999999);
#5023=CIRCLE('',#12379,2.00000000000003);
#5024=CIRCLE('',#12380,2.00000000000003);
#5025=CIRCLE('',#12382,2.00000000000003);
#5026=CIRCLE('',#12383,2.00000000000003);
#5027=CIRCLE('',#12385,2.);
#5028=CIRCLE('',#12386,2.);
#5029=CIRCLE('',#12388,1.49999999999999);
#5030=CIRCLE('',#12389,1.49999999999999);
#5031=CIRCLE('',#12390,1.49999999999999);
#5032=CIRCLE('',#12391,1.49999999999999);
#5033=CIRCLE('',#12392,1.49999999999999);
#5034=CIRCLE('',#12393,1.49999999999999);
#5035=CIRCLE('',#12394,1.49999999999999);
#5036=CIRCLE('',#12395,1.49999999999999);
#5037=CIRCLE('',#12396,1.49999999999999);
#5038=CIRCLE('',#12397,1.49999999999999);
#5039=CIRCLE('',#12398,1.49999999999999);
#5040=CIRCLE('',#12400,4.);
#5041=CIRCLE('',#12401,4.);
#5042=CIRCLE('',#12403,1.49999999999999);
#5043=CIRCLE('',#12404,1.49999999999999);
#5044=CIRCLE('',#12405,1.49999999999999);
#5045=CIRCLE('',#12406,1.49999999999999);
#5046=CIRCLE('',#12407,1.49999999999999);
#5047=CIRCLE('',#12408,1.49999999999999);
#5048=CIRCLE('',#12409,1.49999999999999);
#5049=CIRCLE('',#12410,1.49999999999999);
#5050=CIRCLE('',#12411,1.49999999999999);
#5051=CIRCLE('',#12412,1.49999999999999);
#5052=CIRCLE('',#12413,1.49999999999999);
#5053=CIRCLE('',#12431,1.49999999999999);
#5054=CIRCLE('',#12432,1.49999999999999);
#5055=CIRCLE('',#12433,1.49999999999999);
#5056=CIRCLE('',#12434,1.49999999999999);
#5057=CIRCLE('',#12435,1.49999999999999);
#5058=CIRCLE('',#12436,1.49999999999999);
#5059=CIRCLE('',#12437,1.49999999999999);
#5060=CIRCLE('',#12438,1.49999999999999);
#5061=CIRCLE('',#12439,1.49999999999999);
#5062=CIRCLE('',#12440,1.49999999999999);
#5063=CIRCLE('',#12441,1.49999999999999);
#5064=CIRCLE('',#12443,1.49999999999999);
#5065=CIRCLE('',#12445,1.49999999999999);
#5066=CIRCLE('',#12447,1.49999999999999);
#5067=CIRCLE('',#12449,1.49999999999999);
#5068=CIRCLE('',#12451,1.49999999999999);
#5069=CIRCLE('',#12453,1.49999999999999);
#5070=CIRCLE('',#12455,1.49999999999999);
#5071=CIRCLE('',#12457,1.49999999999999);
#5072=CIRCLE('',#12459,1.49999999999999);
#5073=CIRCLE('',#12461,1.49999999999999);
#5074=CIRCLE('',#12463,1.49999999999999);
#5857=VERTEX_POINT('',#18162);
#5858=VERTEX_POINT('',#18164);
#5859=VERTEX_POINT('',#18168);
#5860=VERTEX_POINT('',#18170);
#5861=VERTEX_POINT('',#18174);
#5862=VERTEX_POINT('',#18176);
#5863=VERTEX_POINT('',#18180);
#5864=VERTEX_POINT('',#18181);
#5865=VERTEX_POINT('',#18183);
#5866=VERTEX_POINT('',#18185);
#5867=VERTEX_POINT('',#18189);
#5868=VERTEX_POINT('',#18191);
#5869=VERTEX_POINT('',#18193);
#5870=VERTEX_POINT('',#18195);
#5871=VERTEX_POINT('',#18197);
#5872=VERTEX_POINT('',#18199);
#5873=VERTEX_POINT('',#18202);
#5874=VERTEX_POINT('',#18204);
#5875=VERTEX_POINT('',#18206);
#5876=VERTEX_POINT('',#18208);
#5877=VERTEX_POINT('',#18210);
#5878=VERTEX_POINT('',#18212);
#5879=VERTEX_POINT('',#18214);
#5880=VERTEX_POINT('',#18216);
#5881=VERTEX_POINT('',#18218);
#5882=VERTEX_POINT('',#18220);
#5883=VERTEX_POINT('',#18222);
#5884=VERTEX_POINT('',#18225);
#5885=VERTEX_POINT('',#18226);
#5886=VERTEX_POINT('',#18228);
#5887=VERTEX_POINT('',#18230);
#5888=VERTEX_POINT('',#18234);
#5889=VERTEX_POINT('',#18236);
#5890=VERTEX_POINT('',#18238);
#5891=VERTEX_POINT('',#18240);
#5892=VERTEX_POINT('',#18242);
#5893=VERTEX_POINT('',#18244);
#5894=VERTEX_POINT('',#18247);
#5895=VERTEX_POINT('',#18249);
#5896=VERTEX_POINT('',#18251);
#5897=VERTEX_POINT('',#18253);
#5898=VERTEX_POINT('',#18255);
#5899=VERTEX_POINT('',#18257);
#5900=VERTEX_POINT('',#18259);
#5901=VERTEX_POINT('',#18261);
#5902=VERTEX_POINT('',#18263);
#5903=VERTEX_POINT('',#18265);
#5904=VERTEX_POINT('',#18267);
#5905=VERTEX_POINT('',#18303);
#5906=VERTEX_POINT('',#18304);
#5907=VERTEX_POINT('',#18306);
#5908=VERTEX_POINT('',#18308);
#5909=VERTEX_POINT('',#18310);
#5910=VERTEX_POINT('',#18312);
#5911=VERTEX_POINT('',#18314);
#5912=VERTEX_POINT('',#18316);
#5913=VERTEX_POINT('',#18319);
#5914=VERTEX_POINT('',#18321);
#5915=VERTEX_POINT('',#18323);
#5916=VERTEX_POINT('',#18325);
#5917=VERTEX_POINT('',#18327);
#5918=VERTEX_POINT('',#18329);
#5919=VERTEX_POINT('',#18331);
#5920=VERTEX_POINT('',#18333);
#5921=VERTEX_POINT('',#18335);
#5922=VERTEX_POINT('',#18337);
#5923=VERTEX_POINT('',#18339);
#5924=VERTEX_POINT('',#18342);
#5925=VERTEX_POINT('',#18346);
#5926=VERTEX_POINT('',#18350);
#5927=VERTEX_POINT('',#18354);
#5928=VERTEX_POINT('',#18358);
#5929=VERTEX_POINT('',#18362);
#5930=VERTEX_POINT('',#18366);
#5931=VERTEX_POINT('',#18370);
#5932=VERTEX_POINT('',#18374);
#5933=VERTEX_POINT('',#18378);
#5934=VERTEX_POINT('',#18382);
#5935=VERTEX_POINT('',#18386);
#5936=VERTEX_POINT('',#18388);
#5937=VERTEX_POINT('',#18392);
#5938=VERTEX_POINT('',#18394);
#5939=VERTEX_POINT('',#18398);
#5940=VERTEX_POINT('',#18402);
#5941=VERTEX_POINT('',#18408);
#5942=VERTEX_POINT('',#18409);
#5943=VERTEX_POINT('',#18414);
#5944=VERTEX_POINT('',#18416);
#5945=VERTEX_POINT('',#18423);
#5946=VERTEX_POINT('',#18427);
#7217=EDGE_CURVE('',#5857,#5857,#5021,.T.);
#7218=EDGE_CURVE('',#5857,#5858,#1349,.T.);
#7219=EDGE_CURVE('',#5858,#5858,#5022,.T.);
#7220=EDGE_CURVE('',#5859,#5859,#5023,.T.);
#7221=EDGE_CURVE('',#5859,#5860,#1350,.T.);
#7222=EDGE_CURVE('',#5860,#5860,#5024,.T.);
#7223=EDGE_CURVE('',#5861,#5861,#5025,.T.);
#7224=EDGE_CURVE('',#5861,#5862,#1351,.T.);
#7225=EDGE_CURVE('',#5862,#5862,#5026,.T.);
#7226=EDGE_CURVE('',#5863,#5864,#5027,.T.);
#7227=EDGE_CURVE('',#5864,#5865,#1352,.T.);
#7228=EDGE_CURVE('',#5865,#5866,#5028,.T.);
#7229=EDGE_CURVE('',#5866,#5863,#1353,.T.);
#7230=EDGE_CURVE('',#5864,#5867,#1354,.T.);
#7231=EDGE_CURVE('',#5868,#5867,#1355,.T.);
#7232=EDGE_CURVE('',#5868,#5869,#1356,.T.);
#7233=EDGE_CURVE('',#5869,#5870,#1357,.T.);
#7234=EDGE_CURVE('',#5871,#5870,#1358,.T.);
#7235=EDGE_CURVE('',#5871,#5872,#1359,.T.);
#7236=EDGE_CURVE('',#5872,#5865,#1360,.T.);
#7237=EDGE_CURVE('',#5873,#5873,#5029,.T.);
#7238=EDGE_CURVE('',#5874,#5874,#5030,.T.);
#7239=EDGE_CURVE('',#5875,#5875,#5031,.T.);
#7240=EDGE_CURVE('',#5876,#5876,#5032,.T.);
#7241=EDGE_CURVE('',#5877,#5877,#5033,.T.);
#7242=EDGE_CURVE('',#5878,#5878,#5034,.T.);
#7243=EDGE_CURVE('',#5879,#5879,#5035,.T.);
#7244=EDGE_CURVE('',#5880,#5880,#5036,.T.);
#7245=EDGE_CURVE('',#5881,#5881,#5037,.T.);
#7246=EDGE_CURVE('',#5882,#5882,#5038,.T.);
#7247=EDGE_CURVE('',#5883,#5883,#5039,.T.);
#7248=EDGE_CURVE('',#5884,#5885,#5040,.T.);
#7249=EDGE_CURVE('',#5885,#5886,#1361,.T.);
#7250=EDGE_CURVE('',#5886,#5887,#5041,.T.);
#7251=EDGE_CURVE('',#5884,#5887,#1362,.T.);
#7252=EDGE_CURVE('',#5885,#5888,#1363,.T.);
#7253=EDGE_CURVE('',#5888,#5889,#1364,.T.);
#7254=EDGE_CURVE('',#5889,#5890,#1365,.T.);
#7255=EDGE_CURVE('',#5890,#5891,#1366,.T.);
#7256=EDGE_CURVE('',#5891,#5892,#1367,.T.);
#7257=EDGE_CURVE('',#5892,#5893,#1368,.T.);
#7258=EDGE_CURVE('',#5893,#5886,#1369,.T.);
#7259=EDGE_CURVE('',#5894,#5894,#5042,.T.);
#7260=EDGE_CURVE('',#5895,#5895,#5043,.T.);
#7261=EDGE_CURVE('',#5896,#5896,#5044,.T.);
#7262=EDGE_CURVE('',#5897,#5897,#5045,.T.);
#7263=EDGE_CURVE('',#5898,#5898,#5046,.T.);
#7264=EDGE_CURVE('',#5899,#5899,#5047,.T.);
#7265=EDGE_CURVE('',#5900,#5900,#5048,.T.);
#7266=EDGE_CURVE('',#5901,#5901,#5049,.T.);
#7267=EDGE_CURVE('',#5902,#5902,#5050,.T.);
#7268=EDGE_CURVE('',#5903,#5903,#5051,.T.);
#7269=EDGE_CURVE('',#5904,#5904,#5052,.T.);
#7270=EDGE_CURVE('',#5894,#5883,#1370,.T.);
#7271=EDGE_CURVE('',#5895,#5882,#1371,.T.);
#7272=EDGE_CURVE('',#5896,#5881,#1372,.T.);
#7273=EDGE_CURVE('',#5897,#5880,#1373,.T.);
#7274=EDGE_CURVE('',#5898,#5879,#1374,.T.);
#7275=EDGE_CURVE('',#5899,#5878,#1375,.T.);
#7276=EDGE_CURVE('',#5900,#5877,#1376,.T.);
#7277=EDGE_CURVE('',#5901,#5876,#1377,.T.);
#7278=EDGE_CURVE('',#5902,#5875,#1378,.T.);
#7279=EDGE_CURVE('',#5903,#5874,#1379,.T.);
#7280=EDGE_CURVE('',#5904,#5873,#1380,.T.);
#7281=EDGE_CURVE('',#5871,#5889,#1381,.T.);
#7282=EDGE_CURVE('',#5872,#5888,#1382,.T.);
#7283=EDGE_CURVE('',#5867,#5893,#1383,.T.);
#7284=EDGE_CURVE('',#5868,#5892,#1384,.T.);
#7285=EDGE_CURVE('',#5869,#5891,#1385,.T.);
#7286=EDGE_CURVE('',#5870,#5890,#1386,.T.);
#7287=EDGE_CURVE('',#5905,#5906,#1387,.T.);
#7288=EDGE_CURVE('',#5905,#5907,#1388,.T.);
#7289=EDGE_CURVE('',#5908,#5907,#1389,.T.);
#7290=EDGE_CURVE('',#5908,#5909,#1390,.T.);
#7291=EDGE_CURVE('',#5909,#5910,#1391,.T.);
#7292=EDGE_CURVE('',#5911,#5910,#1392,.T.);
#7293=EDGE_CURVE('',#5911,#5912,#1393,.T.);
#7294=EDGE_CURVE('',#5912,#5906,#1394,.T.);
#7295=EDGE_CURVE('',#5913,#5913,#5053,.T.);
#7296=EDGE_CURVE('',#5914,#5914,#5054,.T.);
#7297=EDGE_CURVE('',#5915,#5915,#5055,.T.);
#7298=EDGE_CURVE('',#5916,#5916,#5056,.T.);
#7299=EDGE_CURVE('',#5917,#5917,#5057,.T.);
#7300=EDGE_CURVE('',#5918,#5918,#5058,.T.);
#7301=EDGE_CURVE('',#5919,#5919,#5059,.T.);
#7302=EDGE_CURVE('',#5920,#5920,#5060,.T.);
#7303=EDGE_CURVE('',#5921,#5921,#5061,.T.);
#7304=EDGE_CURVE('',#5922,#5922,#5062,.T.);
#7305=EDGE_CURVE('',#5923,#5923,#5063,.T.);
#7306=EDGE_CURVE('',#5924,#5924,#5064,.T.);
#7307=EDGE_CURVE('',#5924,#5913,#1395,.T.);
#7308=EDGE_CURVE('',#5925,#5925,#5065,.T.);
#7309=EDGE_CURVE('',#5925,#5914,#1396,.T.);
#7310=EDGE_CURVE('',#5926,#5926,#5066,.T.);
#7311=EDGE_CURVE('',#5926,#5915,#1397,.T.);
#7312=EDGE_CURVE('',#5927,#5927,#5067,.T.);
#7313=EDGE_CURVE('',#5927,#5916,#1398,.T.);
#7314=EDGE_CURVE('',#5928,#5928,#5068,.T.);
#7315=EDGE_CURVE('',#5928,#5917,#1399,.T.);
#7316=EDGE_CURVE('',#5929,#5929,#5069,.T.);
#7317=EDGE_CURVE('',#5929,#5918,#1400,.T.);
#7318=EDGE_CURVE('',#5930,#5930,#5070,.T.);
#7319=EDGE_CURVE('',#5930,#5919,#1401,.T.);
#7320=EDGE_CURVE('',#5931,#5931,#5071,.T.);
#7321=EDGE_CURVE('',#5931,#5920,#1402,.T.);
#7322=EDGE_CURVE('',#5932,#5932,#5072,.T.);
#7323=EDGE_CURVE('',#5932,#5921,#1403,.T.);
#7324=EDGE_CURVE('',#5933,#5933,#5073,.T.);
#7325=EDGE_CURVE('',#5933,#5922,#1404,.T.);
#7326=EDGE_CURVE('',#5934,#5934,#5074,.T.);
#7327=EDGE_CURVE('',#5934,#5923,#1405,.T.);
#7328=EDGE_CURVE('',#5911,#5935,#1406,.T.);
#7329=EDGE_CURVE('',#5936,#5935,#1407,.T.);
#7330=EDGE_CURVE('',#5912,#5936,#1408,.T.);
#7331=EDGE_CURVE('',#5907,#5937,#1409,.T.);
#7332=EDGE_CURVE('',#5938,#5937,#1410,.T.);
#7333=EDGE_CURVE('',#5908,#5938,#1411,.T.);
#7334=EDGE_CURVE('',#5939,#5938,#1412,.T.);
#7335=EDGE_CURVE('',#5909,#5939,#1413,.T.);
#7336=EDGE_CURVE('',#5940,#5939,#1414,.T.);
#7337=EDGE_CURVE('',#5910,#5940,#1415,.T.);
#7338=EDGE_CURVE('',#5935,#5940,#1416,.T.);
#7339=EDGE_CURVE('',#5941,#5942,#1417,.T.);
#7340=EDGE_CURVE('',#5941,#5936,#1418,.T.);
#7341=EDGE_CURVE('',#5937,#5942,#1419,.T.);
#7342=EDGE_CURVE('',#5884,#5943,#1420,.T.);
#7343=EDGE_CURVE('',#5887,#5944,#1421,.T.);
#7344=EDGE_CURVE('',#5943,#5944,#1422,.T.);
#7345=EDGE_CURVE('',#5866,#5941,#1423,.T.);
#7346=EDGE_CURVE('',#5863,#5942,#1424,.T.);
#7347=EDGE_CURVE('',#5945,#5943,#1425,.T.);
#7348=EDGE_CURVE('',#5906,#5945,#1426,.T.);
#7349=EDGE_CURVE('',#5946,#5945,#1427,.T.);
#7350=EDGE_CURVE('',#5905,#5946,#1428,.T.);
#7351=EDGE_CURVE('',#5944,#5946,#1429,.T.);
#9772=ORIENTED_EDGE('',*,*,#7217,.F.);
#9773=ORIENTED_EDGE('',*,*,#7218,.T.);
#9774=ORIENTED_EDGE('',*,*,#7219,.F.);
#9775=ORIENTED_EDGE('',*,*,#7218,.F.);
#9776=ORIENTED_EDGE('',*,*,#7220,.F.);
#9777=ORIENTED_EDGE('',*,*,#7221,.T.);
#9778=ORIENTED_EDGE('',*,*,#7222,.F.);
#9779=ORIENTED_EDGE('',*,*,#7221,.F.);
#9780=ORIENTED_EDGE('',*,*,#7223,.F.);
#9781=ORIENTED_EDGE('',*,*,#7224,.T.);
#9782=ORIENTED_EDGE('',*,*,#7225,.F.);
#9783=ORIENTED_EDGE('',*,*,#7224,.F.);
#9784=ORIENTED_EDGE('',*,*,#7226,.T.);
#9785=ORIENTED_EDGE('',*,*,#7227,.T.);
#9786=ORIENTED_EDGE('',*,*,#7228,.T.);
#9787=ORIENTED_EDGE('',*,*,#7229,.T.);
#9788=ORIENTED_EDGE('',*,*,#7227,.F.);
#9789=ORIENTED_EDGE('',*,*,#7230,.T.);
#9790=ORIENTED_EDGE('',*,*,#7231,.F.);
#9791=ORIENTED_EDGE('',*,*,#7232,.T.);
#9792=ORIENTED_EDGE('',*,*,#7233,.T.);
#9793=ORIENTED_EDGE('',*,*,#7234,.F.);
#9794=ORIENTED_EDGE('',*,*,#7235,.T.);
#9795=ORIENTED_EDGE('',*,*,#7236,.T.);
#9796=ORIENTED_EDGE('',*,*,#7237,.F.);
#9797=ORIENTED_EDGE('',*,*,#7238,.F.);
#9798=ORIENTED_EDGE('',*,*,#7239,.F.);
#9799=ORIENTED_EDGE('',*,*,#7240,.F.);
#9800=ORIENTED_EDGE('',*,*,#7241,.F.);
#9801=ORIENTED_EDGE('',*,*,#7242,.F.);
#9802=ORIENTED_EDGE('',*,*,#7243,.F.);
#9803=ORIENTED_EDGE('',*,*,#7244,.F.);
#9804=ORIENTED_EDGE('',*,*,#7245,.F.);
#9805=ORIENTED_EDGE('',*,*,#7246,.F.);
#9806=ORIENTED_EDGE('',*,*,#7247,.F.);
#9807=ORIENTED_EDGE('',*,*,#7248,.T.);
#9808=ORIENTED_EDGE('',*,*,#7249,.T.);
#9809=ORIENTED_EDGE('',*,*,#7250,.T.);
#9810=ORIENTED_EDGE('',*,*,#7251,.F.);
#9811=ORIENTED_EDGE('',*,*,#7249,.F.);
#9812=ORIENTED_EDGE('',*,*,#7252,.T.);
#9813=ORIENTED_EDGE('',*,*,#7253,.T.);
#9814=ORIENTED_EDGE('',*,*,#7254,.T.);
#9815=ORIENTED_EDGE('',*,*,#7255,.T.);
#9816=ORIENTED_EDGE('',*,*,#7256,.T.);
#9817=ORIENTED_EDGE('',*,*,#7257,.T.);
#9818=ORIENTED_EDGE('',*,*,#7258,.T.);
#9819=ORIENTED_EDGE('',*,*,#7259,.T.);
#9820=ORIENTED_EDGE('',*,*,#7260,.T.);
#9821=ORIENTED_EDGE('',*,*,#7261,.T.);
#9822=ORIENTED_EDGE('',*,*,#7262,.T.);
#9823=ORIENTED_EDGE('',*,*,#7263,.T.);
#9824=ORIENTED_EDGE('',*,*,#7264,.T.);
#9825=ORIENTED_EDGE('',*,*,#7265,.T.);
#9826=ORIENTED_EDGE('',*,*,#7266,.T.);
#9827=ORIENTED_EDGE('',*,*,#7267,.T.);
#9828=ORIENTED_EDGE('',*,*,#7268,.T.);
#9829=ORIENTED_EDGE('',*,*,#7269,.T.);
#9830=ORIENTED_EDGE('',*,*,#7259,.F.);
#9831=ORIENTED_EDGE('',*,*,#7270,.T.);
#9832=ORIENTED_EDGE('',*,*,#7247,.T.);
#9833=ORIENTED_EDGE('',*,*,#7270,.F.);
#9834=ORIENTED_EDGE('',*,*,#7260,.F.);
#9835=ORIENTED_EDGE('',*,*,#7271,.T.);
#9836=ORIENTED_EDGE('',*,*,#7246,.T.);
#9837=ORIENTED_EDGE('',*,*,#7271,.F.);
#9838=ORIENTED_EDGE('',*,*,#7261,.F.);
#9839=ORIENTED_EDGE('',*,*,#7272,.T.);
#9840=ORIENTED_EDGE('',*,*,#7245,.T.);
#9841=ORIENTED_EDGE('',*,*,#7272,.F.);
#9842=ORIENTED_EDGE('',*,*,#7262,.F.);
#9843=ORIENTED_EDGE('',*,*,#7273,.T.);
#9844=ORIENTED_EDGE('',*,*,#7244,.T.);
#9845=ORIENTED_EDGE('',*,*,#7273,.F.);
#9846=ORIENTED_EDGE('',*,*,#7263,.F.);
#9847=ORIENTED_EDGE('',*,*,#7274,.T.);
#9848=ORIENTED_EDGE('',*,*,#7243,.T.);
#9849=ORIENTED_EDGE('',*,*,#7274,.F.);
#9850=ORIENTED_EDGE('',*,*,#7264,.F.);
#9851=ORIENTED_EDGE('',*,*,#7275,.T.);
#9852=ORIENTED_EDGE('',*,*,#7242,.T.);
#9853=ORIENTED_EDGE('',*,*,#7275,.F.);
#9854=ORIENTED_EDGE('',*,*,#7265,.F.);
#9855=ORIENTED_EDGE('',*,*,#7276,.T.);
#9856=ORIENTED_EDGE('',*,*,#7241,.T.);
#9857=ORIENTED_EDGE('',*,*,#7276,.F.);
#9858=ORIENTED_EDGE('',*,*,#7266,.F.);
#9859=ORIENTED_EDGE('',*,*,#7277,.T.);
#9860=ORIENTED_EDGE('',*,*,#7240,.T.);
#9861=ORIENTED_EDGE('',*,*,#7277,.F.);
#9862=ORIENTED_EDGE('',*,*,#7267,.F.);
#9863=ORIENTED_EDGE('',*,*,#7278,.T.);
#9864=ORIENTED_EDGE('',*,*,#7239,.T.);
#9865=ORIENTED_EDGE('',*,*,#7278,.F.);
#9866=ORIENTED_EDGE('',*,*,#7268,.F.);
#9867=ORIENTED_EDGE('',*,*,#7279,.T.);
#9868=ORIENTED_EDGE('',*,*,#7238,.T.);
#9869=ORIENTED_EDGE('',*,*,#7279,.F.);
#9870=ORIENTED_EDGE('',*,*,#7269,.F.);
#9871=ORIENTED_EDGE('',*,*,#7280,.T.);
#9872=ORIENTED_EDGE('',*,*,#7237,.T.);
#9873=ORIENTED_EDGE('',*,*,#7280,.F.);
#9874=ORIENTED_EDGE('',*,*,#7235,.F.);
#9875=ORIENTED_EDGE('',*,*,#7281,.T.);
#9876=ORIENTED_EDGE('',*,*,#7253,.F.);
#9877=ORIENTED_EDGE('',*,*,#7282,.F.);
#9878=ORIENTED_EDGE('',*,*,#7231,.T.);
#9879=ORIENTED_EDGE('',*,*,#7283,.T.);
#9880=ORIENTED_EDGE('',*,*,#7257,.F.);
#9881=ORIENTED_EDGE('',*,*,#7284,.F.);
#9882=ORIENTED_EDGE('',*,*,#7232,.F.);
#9883=ORIENTED_EDGE('',*,*,#7284,.T.);
#9884=ORIENTED_EDGE('',*,*,#7256,.F.);
#9885=ORIENTED_EDGE('',*,*,#7285,.F.);
#9886=ORIENTED_EDGE('',*,*,#7233,.F.);
#9887=ORIENTED_EDGE('',*,*,#7285,.T.);
#9888=ORIENTED_EDGE('',*,*,#7255,.F.);
#9889=ORIENTED_EDGE('',*,*,#7286,.F.);
#9890=ORIENTED_EDGE('',*,*,#7234,.T.);
#9891=ORIENTED_EDGE('',*,*,#7286,.T.);
#9892=ORIENTED_EDGE('',*,*,#7254,.F.);
#9893=ORIENTED_EDGE('',*,*,#7281,.F.);
#9894=ORIENTED_EDGE('',*,*,#7287,.F.);
#9895=ORIENTED_EDGE('',*,*,#7288,.T.);
#9896=ORIENTED_EDGE('',*,*,#7289,.F.);
#9897=ORIENTED_EDGE('',*,*,#7290,.T.);
#9898=ORIENTED_EDGE('',*,*,#7291,.T.);
#9899=ORIENTED_EDGE('',*,*,#7292,.F.);
#9900=ORIENTED_EDGE('',*,*,#7293,.T.);
#9901=ORIENTED_EDGE('',*,*,#7294,.T.);
#9902=ORIENTED_EDGE('',*,*,#7295,.F.);
#9903=ORIENTED_EDGE('',*,*,#7296,.F.);
#9904=ORIENTED_EDGE('',*,*,#7297,.F.);
#9905=ORIENTED_EDGE('',*,*,#7298,.F.);
#9906=ORIENTED_EDGE('',*,*,#7299,.F.);
#9907=ORIENTED_EDGE('',*,*,#7300,.F.);
#9908=ORIENTED_EDGE('',*,*,#7301,.F.);
#9909=ORIENTED_EDGE('',*,*,#7302,.F.);
#9910=ORIENTED_EDGE('',*,*,#7303,.F.);
#9911=ORIENTED_EDGE('',*,*,#7304,.F.);
#9912=ORIENTED_EDGE('',*,*,#7305,.F.);
#9913=ORIENTED_EDGE('',*,*,#7306,.F.);
#9914=ORIENTED_EDGE('',*,*,#7307,.T.);
#9915=ORIENTED_EDGE('',*,*,#7295,.T.);
#9916=ORIENTED_EDGE('',*,*,#7307,.F.);
#9917=ORIENTED_EDGE('',*,*,#7308,.F.);
#9918=ORIENTED_EDGE('',*,*,#7309,.T.);
#9919=ORIENTED_EDGE('',*,*,#7296,.T.);
#9920=ORIENTED_EDGE('',*,*,#7309,.F.);
#9921=ORIENTED_EDGE('',*,*,#7310,.F.);
#9922=ORIENTED_EDGE('',*,*,#7311,.T.);
#9923=ORIENTED_EDGE('',*,*,#7297,.T.);
#9924=ORIENTED_EDGE('',*,*,#7311,.F.);
#9925=ORIENTED_EDGE('',*,*,#7312,.F.);
#9926=ORIENTED_EDGE('',*,*,#7313,.T.);
#9927=ORIENTED_EDGE('',*,*,#7298,.T.);
#9928=ORIENTED_EDGE('',*,*,#7313,.F.);
#9929=ORIENTED_EDGE('',*,*,#7314,.F.);
#9930=ORIENTED_EDGE('',*,*,#7315,.T.);
#9931=ORIENTED_EDGE('',*,*,#7299,.T.);
#9932=ORIENTED_EDGE('',*,*,#7315,.F.);
#9933=ORIENTED_EDGE('',*,*,#7316,.F.);
#9934=ORIENTED_EDGE('',*,*,#7317,.T.);
#9935=ORIENTED_EDGE('',*,*,#7300,.T.);
#9936=ORIENTED_EDGE('',*,*,#7317,.F.);
#9937=ORIENTED_EDGE('',*,*,#7318,.F.);
#9938=ORIENTED_EDGE('',*,*,#7319,.T.);
#9939=ORIENTED_EDGE('',*,*,#7301,.T.);
#9940=ORIENTED_EDGE('',*,*,#7319,.F.);
#9941=ORIENTED_EDGE('',*,*,#7320,.F.);
#9942=ORIENTED_EDGE('',*,*,#7321,.T.);
#9943=ORIENTED_EDGE('',*,*,#7302,.T.);
#9944=ORIENTED_EDGE('',*,*,#7321,.F.);
#9945=ORIENTED_EDGE('',*,*,#7322,.F.);
#9946=ORIENTED_EDGE('',*,*,#7323,.T.);
#9947=ORIENTED_EDGE('',*,*,#7303,.T.);
#9948=ORIENTED_EDGE('',*,*,#7323,.F.);
#9949=ORIENTED_EDGE('',*,*,#7324,.F.);
#9950=ORIENTED_EDGE('',*,*,#7325,.T.);
#9951=ORIENTED_EDGE('',*,*,#7304,.T.);
#9952=ORIENTED_EDGE('',*,*,#7325,.F.);
#9953=ORIENTED_EDGE('',*,*,#7326,.F.);
#9954=ORIENTED_EDGE('',*,*,#7327,.T.);
#9955=ORIENTED_EDGE('',*,*,#7305,.T.);
#9956=ORIENTED_EDGE('',*,*,#7327,.F.);
#9957=ORIENTED_EDGE('',*,*,#7293,.F.);
#9958=ORIENTED_EDGE('',*,*,#7328,.T.);
#9959=ORIENTED_EDGE('',*,*,#7329,.F.);
#9960=ORIENTED_EDGE('',*,*,#7330,.F.);
#9961=ORIENTED_EDGE('',*,*,#7289,.T.);
#9962=ORIENTED_EDGE('',*,*,#7331,.T.);
#9963=ORIENTED_EDGE('',*,*,#7332,.F.);
#9964=ORIENTED_EDGE('',*,*,#7333,.F.);
#9965=ORIENTED_EDGE('',*,*,#7290,.F.);
#9966=ORIENTED_EDGE('',*,*,#7333,.T.);
#9967=ORIENTED_EDGE('',*,*,#7334,.F.);
#9968=ORIENTED_EDGE('',*,*,#7335,.F.);
#9969=ORIENTED_EDGE('',*,*,#7291,.F.);
#9970=ORIENTED_EDGE('',*,*,#7335,.T.);
#9971=ORIENTED_EDGE('',*,*,#7336,.F.);
#9972=ORIENTED_EDGE('',*,*,#7337,.F.);
#9973=ORIENTED_EDGE('',*,*,#7292,.T.);
#9974=ORIENTED_EDGE('',*,*,#7337,.T.);
#9975=ORIENTED_EDGE('',*,*,#7338,.F.);
#9976=ORIENTED_EDGE('',*,*,#7328,.F.);
#9977=ORIENTED_EDGE('',*,*,#7339,.F.);
#9978=ORIENTED_EDGE('',*,*,#7340,.T.);
#9979=ORIENTED_EDGE('',*,*,#7329,.T.);
#9980=ORIENTED_EDGE('',*,*,#7338,.T.);
#9981=ORIENTED_EDGE('',*,*,#7336,.T.);
#9982=ORIENTED_EDGE('',*,*,#7334,.T.);
#9983=ORIENTED_EDGE('',*,*,#7332,.T.);
#9984=ORIENTED_EDGE('',*,*,#7341,.T.);
#9985=ORIENTED_EDGE('',*,*,#7306,.T.);
#9986=ORIENTED_EDGE('',*,*,#7308,.T.);
#9987=ORIENTED_EDGE('',*,*,#7310,.T.);
#9988=ORIENTED_EDGE('',*,*,#7312,.T.);
#9989=ORIENTED_EDGE('',*,*,#7314,.T.);
#9990=ORIENTED_EDGE('',*,*,#7316,.T.);
#9991=ORIENTED_EDGE('',*,*,#7318,.T.);
#9992=ORIENTED_EDGE('',*,*,#7320,.T.);
#9993=ORIENTED_EDGE('',*,*,#7322,.T.);
#9994=ORIENTED_EDGE('',*,*,#7324,.T.);
#9995=ORIENTED_EDGE('',*,*,#7326,.T.);
#9996=ORIENTED_EDGE('',*,*,#7342,.F.);
#9997=ORIENTED_EDGE('',*,*,#7251,.T.);
#9998=ORIENTED_EDGE('',*,*,#7343,.T.);
#9999=ORIENTED_EDGE('',*,*,#7344,.F.);
#10000=ORIENTED_EDGE('',*,*,#7219,.T.);
#10001=ORIENTED_EDGE('',*,*,#7220,.T.);
#10002=ORIENTED_EDGE('',*,*,#7223,.T.);
#10003=ORIENTED_EDGE('',*,*,#7229,.F.);
#10004=ORIENTED_EDGE('',*,*,#7345,.T.);
#10005=ORIENTED_EDGE('',*,*,#7339,.T.);
#10006=ORIENTED_EDGE('',*,*,#7346,.F.);
#10007=ORIENTED_EDGE('',*,*,#7217,.T.);
#10008=ORIENTED_EDGE('',*,*,#7342,.T.);
#10009=ORIENTED_EDGE('',*,*,#7347,.F.);
#10010=ORIENTED_EDGE('',*,*,#7348,.F.);
#10011=ORIENTED_EDGE('',*,*,#7294,.F.);
#10012=ORIENTED_EDGE('',*,*,#7330,.T.);
#10013=ORIENTED_EDGE('',*,*,#7340,.F.);
#10014=ORIENTED_EDGE('',*,*,#7345,.F.);
#10015=ORIENTED_EDGE('',*,*,#7228,.F.);
#10016=ORIENTED_EDGE('',*,*,#7236,.F.);
#10017=ORIENTED_EDGE('',*,*,#7282,.T.);
#10018=ORIENTED_EDGE('',*,*,#7252,.F.);
#10019=ORIENTED_EDGE('',*,*,#7248,.F.);
#10020=ORIENTED_EDGE('',*,*,#7287,.T.);
#10021=ORIENTED_EDGE('',*,*,#7348,.T.);
#10022=ORIENTED_EDGE('',*,*,#7349,.F.);
#10023=ORIENTED_EDGE('',*,*,#7350,.F.);
#10024=ORIENTED_EDGE('',*,*,#7222,.T.);
#10025=ORIENTED_EDGE('',*,*,#7225,.T.);
#10026=ORIENTED_EDGE('',*,*,#7343,.F.);
#10027=ORIENTED_EDGE('',*,*,#7250,.F.);
#10028=ORIENTED_EDGE('',*,*,#7258,.F.);
#10029=ORIENTED_EDGE('',*,*,#7283,.F.);
#10030=ORIENTED_EDGE('',*,*,#7230,.F.);
#10031=ORIENTED_EDGE('',*,*,#7226,.F.);
#10032=ORIENTED_EDGE('',*,*,#7346,.T.);
#10033=ORIENTED_EDGE('',*,*,#7341,.F.);
#10034=ORIENTED_EDGE('',*,*,#7331,.F.);
#10035=ORIENTED_EDGE('',*,*,#7288,.F.);
#10036=ORIENTED_EDGE('',*,*,#7350,.T.);
#10037=ORIENTED_EDGE('',*,*,#7351,.F.);
#10038=ORIENTED_EDGE('',*,*,#7344,.T.);
#10039=ORIENTED_EDGE('',*,*,#7351,.T.);
#10040=ORIENTED_EDGE('',*,*,#7349,.T.);
#10041=ORIENTED_EDGE('',*,*,#7347,.T.);
#11132=ADVANCED_FACE('',(#3256),#2801,.F.);
#11133=ADVANCED_FACE('',(#3257),#2802,.F.);
#11134=ADVANCED_FACE('',(#3258),#2803,.F.);
#11135=ADVANCED_FACE('',(#3259),#2804,.F.);
#11136=ADVANCED_FACE('',(#3260,#515,#516,#517,#518,#519,#520,#521,#522,
#523,#524,#525),#732,.F.);
#11137=ADVANCED_FACE('',(#3261),#2805,.T.);
#11138=ADVANCED_FACE('',(#3262,#526,#527,#528,#529,#530,#531,#532,#533,
#534,#535,#536),#733,.T.);
#11139=ADVANCED_FACE('',(#3263),#2806,.F.);
#11140=ADVANCED_FACE('',(#3264),#2807,.F.);
#11141=ADVANCED_FACE('',(#3265),#2808,.F.);
#11142=ADVANCED_FACE('',(#3266),#2809,.F.);
#11143=ADVANCED_FACE('',(#3267),#2810,.F.);
#11144=ADVANCED_FACE('',(#3268),#2811,.F.);
#11145=ADVANCED_FACE('',(#3269),#2812,.F.);
#11146=ADVANCED_FACE('',(#3270),#2813,.F.);
#11147=ADVANCED_FACE('',(#3271),#2814,.F.);
#11148=ADVANCED_FACE('',(#3272),#2815,.F.);
#11149=ADVANCED_FACE('',(#3273),#2816,.F.);
#11150=ADVANCED_FACE('',(#3274),#734,.T.);
#11151=ADVANCED_FACE('',(#3275),#735,.T.);
#11152=ADVANCED_FACE('',(#3276),#736,.T.);
#11153=ADVANCED_FACE('',(#3277),#737,.T.);
#11154=ADVANCED_FACE('',(#3278),#738,.T.);
#11155=ADVANCED_FACE('',(#3279,#537,#538,#539,#540,#541,#542,#543,#544,
#545,#546,#547),#739,.F.);
#11156=ADVANCED_FACE('',(#3280),#2817,.F.);
#11157=ADVANCED_FACE('',(#3281),#2818,.F.);
#11158=ADVANCED_FACE('',(#3282),#2819,.F.);
#11159=ADVANCED_FACE('',(#3283),#2820,.F.);
#11160=ADVANCED_FACE('',(#3284),#2821,.F.);
#11161=ADVANCED_FACE('',(#3285),#2822,.F.);
#11162=ADVANCED_FACE('',(#3286),#2823,.F.);
#11163=ADVANCED_FACE('',(#3287),#2824,.F.);
#11164=ADVANCED_FACE('',(#3288),#2825,.F.);
#11165=ADVANCED_FACE('',(#3289),#2826,.F.);
#11166=ADVANCED_FACE('',(#3290),#2827,.F.);
#11167=ADVANCED_FACE('',(#3291),#740,.T.);
#11168=ADVANCED_FACE('',(#3292),#741,.T.);
#11169=ADVANCED_FACE('',(#3293),#742,.T.);
#11170=ADVANCED_FACE('',(#3294),#743,.T.);
#11171=ADVANCED_FACE('',(#3295),#744,.T.);
#11172=ADVANCED_FACE('',(#3296,#548,#549,#550,#551,#552,#553,#554,#555,
#556,#557,#558),#745,.T.);
#11173=ADVANCED_FACE('',(#3297,#559,#560,#561),#746,.T.);
#11174=ADVANCED_FACE('',(#3298,#562),#747,.T.);
#11175=ADVANCED_FACE('',(#3299),#748,.T.);
#11176=ADVANCED_FACE('',(#3300,#563,#564),#749,.T.);
#11177=ADVANCED_FACE('',(#3301),#750,.T.);
#11178=ADVANCED_FACE('',(#3302),#751,.T.);
#11320=CLOSED_SHELL('',(#11132,#11133,#11134,#11135,#11136,#11137,#11138,
#11139,#11140,#11141,#11142,#11143,#11144,#11145,#11146,#11147,#11148,#11149,
#11150,#11151,#11152,#11153,#11154,#11155,#11156,#11157,#11158,#11159,#11160,
#11161,#11162,#11163,#11164,#11165,#11166,#11167,#11168,#11169,#11170,#11171,
#11172,#11173,#11174,#11175,#11176,#11177,#11178));
#12374=AXIS2_PLACEMENT_3D('',#18160,#15020,#15021);
#12375=AXIS2_PLACEMENT_3D('',#18161,#15022,#15023);
#12376=AXIS2_PLACEMENT_3D('',#18163,#15024,#15025);
#12377=AXIS2_PLACEMENT_3D('',#18166,#15027,#15028);
#12378=AXIS2_PLACEMENT_3D('',#18167,#15029,#15030);
#12379=AXIS2_PLACEMENT_3D('',#18169,#15031,#15032);
#12380=AXIS2_PLACEMENT_3D('',#18172,#15034,#15035);
#12381=AXIS2_PLACEMENT_3D('',#18173,#15036,#15037);
#12382=AXIS2_PLACEMENT_3D('',#18175,#15038,#15039);
#12383=AXIS2_PLACEMENT_3D('',#18178,#15041,#15042);
#12384=AXIS2_PLACEMENT_3D('',#18179,#15043,#15044);
#12385=AXIS2_PLACEMENT_3D('',#18182,#15045,#15046);
#12386=AXIS2_PLACEMENT_3D('',#18186,#15048,#15049);
#12387=AXIS2_PLACEMENT_3D('',#18188,#15051,#15052);
#12388=AXIS2_PLACEMENT_3D('',#18203,#15060,#15061);
#12389=AXIS2_PLACEMENT_3D('',#18205,#15062,#15063);
#12390=AXIS2_PLACEMENT_3D('',#18207,#15064,#15065);
#12391=AXIS2_PLACEMENT_3D('',#18209,#15066,#15067);
#12392=AXIS2_PLACEMENT_3D('',#18211,#15068,#15069);
#12393=AXIS2_PLACEMENT_3D('',#18213,#15070,#15071);
#12394=AXIS2_PLACEMENT_3D('',#18215,#15072,#15073);
#12395=AXIS2_PLACEMENT_3D('',#18217,#15074,#15075);
#12396=AXIS2_PLACEMENT_3D('',#18219,#15076,#15077);
#12397=AXIS2_PLACEMENT_3D('',#18221,#15078,#15079);
#12398=AXIS2_PLACEMENT_3D('',#18223,#15080,#15081);
#12399=AXIS2_PLACEMENT_3D('',#18224,#15082,#15083);
#12400=AXIS2_PLACEMENT_3D('',#18227,#15084,#15085);
#12401=AXIS2_PLACEMENT_3D('',#18231,#15087,#15088);
#12402=AXIS2_PLACEMENT_3D('',#18233,#15090,#15091);
#12403=AXIS2_PLACEMENT_3D('',#18248,#15099,#15100);
#12404=AXIS2_PLACEMENT_3D('',#18250,#15101,#15102);
#12405=AXIS2_PLACEMENT_3D('',#18252,#15103,#15104);
#12406=AXIS2_PLACEMENT_3D('',#18254,#15105,#15106);
#12407=AXIS2_PLACEMENT_3D('',#18256,#15107,#15108);
#12408=AXIS2_PLACEMENT_3D('',#18258,#15109,#15110);
#12409=AXIS2_PLACEMENT_3D('',#18260,#15111,#15112);
#12410=AXIS2_PLACEMENT_3D('',#18262,#15113,#15114);
#12411=AXIS2_PLACEMENT_3D('',#18264,#15115,#15116);
#12412=AXIS2_PLACEMENT_3D('',#18266,#15117,#15118);
#12413=AXIS2_PLACEMENT_3D('',#18268,#15119,#15120);
#12414=AXIS2_PLACEMENT_3D('',#18269,#15121,#15122);
#12415=AXIS2_PLACEMENT_3D('',#18271,#15124,#15125);
#12416=AXIS2_PLACEMENT_3D('',#18273,#15127,#15128);
#12417=AXIS2_PLACEMENT_3D('',#18275,#15130,#15131);
#12418=AXIS2_PLACEMENT_3D('',#18277,#15133,#15134);
#12419=AXIS2_PLACEMENT_3D('',#18279,#15136,#15137);
#12420=AXIS2_PLACEMENT_3D('',#18281,#15139,#15140);
#12421=AXIS2_PLACEMENT_3D('',#18283,#15142,#15143);
#12422=AXIS2_PLACEMENT_3D('',#18285,#15145,#15146);
#12423=AXIS2_PLACEMENT_3D('',#18287,#15148,#15149);
#12424=AXIS2_PLACEMENT_3D('',#18289,#15151,#15152);
#12425=AXIS2_PLACEMENT_3D('',#18291,#15154,#15155);
#12426=AXIS2_PLACEMENT_3D('',#18294,#15158,#15159);
#12427=AXIS2_PLACEMENT_3D('',#18297,#15162,#15163);
#12428=AXIS2_PLACEMENT_3D('',#18299,#15165,#15166);
#12429=AXIS2_PLACEMENT_3D('',#18301,#15168,#15169);
#12430=AXIS2_PLACEMENT_3D('',#18302,#15170,#15171);
#12431=AXIS2_PLACEMENT_3D('',#18320,#15180,#15181);
#12432=AXIS2_PLACEMENT_3D('',#18322,#15182,#15183);
#12433=AXIS2_PLACEMENT_3D('',#18324,#15184,#15185);
#12434=AXIS2_PLACEMENT_3D('',#18326,#15186,#15187);
#12435=AXIS2_PLACEMENT_3D('',#18328,#15188,#15189);
#12436=AXIS2_PLACEMENT_3D('',#18330,#15190,#15191);
#12437=AXIS2_PLACEMENT_3D('',#18332,#15192,#15193);
#12438=AXIS2_PLACEMENT_3D('',#18334,#15194,#15195);
#12439=AXIS2_PLACEMENT_3D('',#18336,#15196,#15197);
#12440=AXIS2_PLACEMENT_3D('',#18338,#15198,#15199);
#12441=AXIS2_PLACEMENT_3D('',#18340,#15200,#15201);
#12442=AXIS2_PLACEMENT_3D('',#18341,#15202,#15203);
#12443=AXIS2_PLACEMENT_3D('',#18343,#15204,#15205);
#12444=AXIS2_PLACEMENT_3D('',#18345,#15207,#15208);
#12445=AXIS2_PLACEMENT_3D('',#18347,#15209,#15210);
#12446=AXIS2_PLACEMENT_3D('',#18349,#15212,#15213);
#12447=AXIS2_PLACEMENT_3D('',#18351,#15214,#15215);
#12448=AXIS2_PLACEMENT_3D('',#18353,#15217,#15218);
#12449=AXIS2_PLACEMENT_3D('',#18355,#15219,#15220);
#12450=AXIS2_PLACEMENT_3D('',#18357,#15222,#15223);
#12451=AXIS2_PLACEMENT_3D('',#18359,#15224,#15225);
#12452=AXIS2_PLACEMENT_3D('',#18361,#15227,#15228);
#12453=AXIS2_PLACEMENT_3D('',#18363,#15229,#15230);
#12454=AXIS2_PLACEMENT_3D('',#18365,#15232,#15233);
#12455=AXIS2_PLACEMENT_3D('',#18367,#15234,#15235);
#12456=AXIS2_PLACEMENT_3D('',#18369,#15237,#15238);
#12457=AXIS2_PLACEMENT_3D('',#18371,#15239,#15240);
#12458=AXIS2_PLACEMENT_3D('',#18373,#15242,#15243);
#12459=AXIS2_PLACEMENT_3D('',#18375,#15244,#15245);
#12460=AXIS2_PLACEMENT_3D('',#18377,#15247,#15248);
#12461=AXIS2_PLACEMENT_3D('',#18379,#15249,#15250);
#12462=AXIS2_PLACEMENT_3D('',#18381,#15252,#15253);
#12463=AXIS2_PLACEMENT_3D('',#18383,#15254,#15255);
#12464=AXIS2_PLACEMENT_3D('',#18385,#15257,#15258);
#12465=AXIS2_PLACEMENT_3D('',#18391,#15262,#15263);
#12466=AXIS2_PLACEMENT_3D('',#18397,#15267,#15268);
#12467=AXIS2_PLACEMENT_3D('',#18401,#15271,#15272);
#12468=AXIS2_PLACEMENT_3D('',#18405,#15275,#15276);
#12469=AXIS2_PLACEMENT_3D('',#18407,#15278,#15279);
#12470=AXIS2_PLACEMENT_3D('',#18413,#15283,#15284);
#12471=AXIS2_PLACEMENT_3D('',#18419,#15288,#15289);
#12472=AXIS2_PLACEMENT_3D('',#18422,#15292,#15293);
#12473=AXIS2_PLACEMENT_3D('',#18426,#15296,#15297);
#12474=AXIS2_PLACEMENT_3D('',#18430,#15300,#15301);
#12475=AXIS2_PLACEMENT_3D('',#18432,#15303,#15304);
#15020=DIRECTION('axis',(0.,0.,1.));
#15021=DIRECTION('refdir',(1.,0.,0.));
#15022=DIRECTION('center_axis',(0.,1.,0.));
#15023=DIRECTION('ref_axis',(1.,0.,0.));
#15024=DIRECTION('center_axis',(0.,1.,0.));
#15025=DIRECTION('ref_axis',(1.,0.,0.));
#15026=DIRECTION('',(0.,1.,0.));
#15027=DIRECTION('center_axis',(0.,-1.,0.));
#15028=DIRECTION('ref_axis',(1.,0.,0.));
#15029=DIRECTION('center_axis',(0.,-1.,0.));
#15030=DIRECTION('ref_axis',(-1.,0.,0.));
#15031=DIRECTION('center_axis',(0.,-1.,0.));
#15032=DIRECTION('ref_axis',(-1.,0.,0.));
#15033=DIRECTION('',(0.,-1.,0.));
#15034=DIRECTION('center_axis',(0.,1.,0.));
#15035=DIRECTION('ref_axis',(-1.,0.,0.));
#15036=DIRECTION('center_axis',(0.,-1.,0.));
#15037=DIRECTION('ref_axis',(-1.,0.,0.));
#15038=DIRECTION('center_axis',(0.,-1.,0.));
#15039=DIRECTION('ref_axis',(-1.,0.,0.));
#15040=DIRECTION('',(0.,-1.,0.));
#15041=DIRECTION('center_axis',(0.,1.,0.));
#15042=DIRECTION('ref_axis',(-1.,0.,0.));
#15043=DIRECTION('center_axis',(-1.,0.,0.));
#15044=DIRECTION('ref_axis',(0.,0.707106781186546,0.707106781186549));
#15045=DIRECTION('center_axis',(1.,0.,0.));
#15046=DIRECTION('ref_axis',(0.,0.707106781186546,0.707106781186549));
#15047=DIRECTION('',(-1.,0.,0.));
#15048=DIRECTION('center_axis',(-1.,0.,0.));
#15049=DIRECTION('ref_axis',(0.,0.707106781186546,0.707106781186549));
#15050=DIRECTION('',(1.,0.,0.));
#15051=DIRECTION('center_axis',(0.,0.,1.));
#15052=DIRECTION('ref_axis',(1.,0.,0.));
#15053=DIRECTION('',(0.,-1.,0.));
#15054=DIRECTION('',(-0.707106781186546,0.707106781186549,0.));
#15055=DIRECTION('',(-0.707106781186546,-0.707106781186549,0.));
#15056=DIRECTION('',(-1.,0.,0.));
#15057=DIRECTION('',(0.707106781186546,-0.707106781186549,0.));
#15058=DIRECTION('',(0.707106781186546,0.707106781186549,0.));
#15059=DIRECTION('',(0.,1.,0.));
#15060=DIRECTION('center_axis',(0.,0.,-1.));
#15061=DIRECTION('ref_axis',(1.,0.,0.));
#15062=DIRECTION('center_axis',(0.,0.,-1.));
#15063=DIRECTION('ref_axis',(1.,0.,0.));
#15064=DIRECTION('center_axis',(0.,0.,-1.));
#15065=DIRECTION('ref_axis',(1.,0.,0.));
#15066=DIRECTION('center_axis',(0.,0.,-1.));
#15067=DIRECTION('ref_axis',(1.,0.,0.));
#15068=DIRECTION('center_axis',(0.,0.,-1.));
#15069=DIRECTION('ref_axis',(1.,0.,0.));
#15070=DIRECTION('center_axis',(0.,0.,-1.));
#15071=DIRECTION('ref_axis',(1.,0.,0.));
#15072=DIRECTION('center_axis',(0.,0.,-1.));
#15073=DIRECTION('ref_axis',(1.,0.,0.));
#15074=DIRECTION('center_axis',(0.,0.,-1.));
#15075=DIRECTION('ref_axis',(1.,0.,0.));
#15076=DIRECTION('center_axis',(0.,0.,-1.));
#15077=DIRECTION('ref_axis',(1.,0.,0.));
#15078=DIRECTION('center_axis',(0.,0.,-1.));
#15079=DIRECTION('ref_axis',(1.,0.,0.));
#15080=DIRECTION('center_axis',(0.,0.,-1.));
#15081=DIRECTION('ref_axis',(1.,0.,0.));
#15082=DIRECTION('center_axis',(1.,0.,0.));
#15083=DIRECTION('ref_axis',(0.,0.992156741649222,0.125));
#15084=DIRECTION('center_axis',(1.,0.,0.));
#15085=DIRECTION('ref_axis',(0.,0.992156741649222,0.125));
#15086=DIRECTION('',(1.,0.,0.));
#15087=DIRECTION('center_axis',(-1.,0.,0.));
#15088=DIRECTION('ref_axis',(0.,0.992156741649222,0.125));
#15089=DIRECTION('',(1.,0.,0.));
#15090=DIRECTION('center_axis',(0.,0.,1.));
#15091=DIRECTION('ref_axis',(1.,0.,0.));
#15092=DIRECTION('',(0.,-1.,0.));
#15093=DIRECTION('',(-0.707106781186546,-0.707106781186549,0.));
#15094=DIRECTION('',(0.707106781186546,-0.707106781186549,0.));
#15095=DIRECTION('',(1.,0.,0.));
#15096=DIRECTION('',(0.707106781186546,0.707106781186549,0.));
#15097=DIRECTION('',(-0.707106781186546,0.707106781186549,0.));
#15098=DIRECTION('',(0.,1.,0.));
#15099=DIRECTION('center_axis',(0.,0.,-1.));
#15100=DIRECTION('ref_axis',(1.,0.,0.));
#15101=DIRECTION('center_axis',(0.,0.,-1.));
#15102=DIRECTION('ref_axis',(1.,0.,0.));
#15103=DIRECTION('center_axis',(0.,0.,-1.));
#15104=DIRECTION('ref_axis',(1.,0.,0.));
#15105=DIRECTION('center_axis',(0.,0.,-1.));
#15106=DIRECTION('ref_axis',(1.,0.,0.));
#15107=DIRECTION('center_axis',(0.,0.,-1.));
#15108=DIRECTION('ref_axis',(1.,0.,0.));
#15109=DIRECTION('center_axis',(0.,0.,-1.));
#15110=DIRECTION('ref_axis',(1.,0.,0.));
#15111=DIRECTION('center_axis',(0.,0.,-1.));
#15112=DIRECTION('ref_axis',(1.,0.,0.));
#15113=DIRECTION('center_axis',(0.,0.,-1.));
#15114=DIRECTION('ref_axis',(1.,0.,0.));
#15115=DIRECTION('center_axis',(0.,0.,-1.));
#15116=DIRECTION('ref_axis',(1.,0.,0.));
#15117=DIRECTION('center_axis',(0.,0.,-1.));
#15118=DIRECTION('ref_axis',(1.,0.,0.));
#15119=DIRECTION('center_axis',(0.,0.,-1.));
#15120=DIRECTION('ref_axis',(1.,0.,0.));
#15121=DIRECTION('center_axis',(0.,0.,1.));
#15122=DIRECTION('ref_axis',(1.,0.,0.));
#15123=DIRECTION('',(0.,0.,-1.));
#15124=DIRECTION('center_axis',(0.,0.,1.));
#15125=DIRECTION('ref_axis',(1.,0.,0.));
#15126=DIRECTION('',(0.,0.,-1.));
#15127=DIRECTION('center_axis',(0.,0.,1.));
#15128=DIRECTION('ref_axis',(1.,0.,0.));
#15129=DIRECTION('',(0.,0.,-1.));
#15130=DIRECTION('center_axis',(0.,0.,1.));
#15131=DIRECTION('ref_axis',(1.,0.,0.));
#15132=DIRECTION('',(0.,0.,-1.));
#15133=DIRECTION('center_axis',(0.,0.,1.));
#15134=DIRECTION('ref_axis',(1.,0.,0.));
#15135=DIRECTION('',(0.,0.,-1.));
#15136=DIRECTION('center_axis',(0.,0.,1.));
#15137=DIRECTION('ref_axis',(1.,0.,0.));
#15138=DIRECTION('',(0.,0.,-1.));
#15139=DIRECTION('center_axis',(0.,0.,1.));
#15140=DIRECTION('ref_axis',(1.,0.,0.));
#15141=DIRECTION('',(0.,0.,-1.));
#15142=DIRECTION('center_axis',(0.,0.,1.));
#15143=DIRECTION('ref_axis',(1.,0.,0.));
#15144=DIRECTION('',(0.,0.,-1.));
#15145=DIRECTION('center_axis',(0.,0.,1.));
#15146=DIRECTION('ref_axis',(1.,0.,0.));
#15147=DIRECTION('',(0.,0.,-1.));
#15148=DIRECTION('center_axis',(0.,0.,1.));
#15149=DIRECTION('ref_axis',(1.,0.,0.));
#15150=DIRECTION('',(0.,0.,-1.));
#15151=DIRECTION('center_axis',(0.,0.,1.));
#15152=DIRECTION('ref_axis',(1.,0.,0.));
#15153=DIRECTION('',(0.,0.,-1.));
#15154=DIRECTION('center_axis',(-0.707106781186549,0.707106781186546,0.));
#15155=DIRECTION('ref_axis',(-0.707106781186546,-0.707106781186549,0.));
#15156=DIRECTION('',(0.,0.,1.));
#15157=DIRECTION('',(0.,0.,1.));
#15158=DIRECTION('center_axis',(0.707106781186549,0.707106781186546,0.));
#15159=DIRECTION('ref_axis',(-0.707106781186546,0.707106781186549,0.));
#15160=DIRECTION('',(0.,0.,1.));
#15161=DIRECTION('',(0.,0.,1.));
#15162=DIRECTION('center_axis',(0.707106781186549,-0.707106781186546,0.));
#15163=DIRECTION('ref_axis',(0.707106781186546,0.707106781186549,0.));
#15164=DIRECTION('',(0.,0.,1.));
#15165=DIRECTION('center_axis',(0.,-1.,0.));
#15166=DIRECTION('ref_axis',(1.,0.,0.));
#15167=DIRECTION('',(0.,0.,1.));
#15168=DIRECTION('center_axis',(-0.707106781186549,-0.707106781186546,0.));
#15169=DIRECTION('ref_axis',(0.707106781186546,-0.707106781186549,0.));
#15170=DIRECTION('center_axis',(0.,0.,1.));
#15171=DIRECTION('ref_axis',(1.,0.,0.));
#15172=DIRECTION('',(-1.,0.,0.));
#15173=DIRECTION('',(0.,-1.,0.));
#15174=DIRECTION('',(-0.707106781186546,0.707106781186549,0.));
#15175=DIRECTION('',(-0.707106781186546,-0.707106781186549,0.));
#15176=DIRECTION('',(-1.,0.,0.));
#15177=DIRECTION('',(0.707106781186546,-0.707106781186549,0.));
#15178=DIRECTION('',(0.707106781186546,0.707106781186549,0.));
#15179=DIRECTION('',(0.,1.,0.));
#15180=DIRECTION('center_axis',(0.,0.,-1.));
#15181=DIRECTION('ref_axis',(1.,0.,0.));
#15182=DIRECTION('center_axis',(0.,0.,-1.));
#15183=DIRECTION('ref_axis',(1.,0.,0.));
#15184=DIRECTION('center_axis',(0.,0.,-1.));
#15185=DIRECTION('ref_axis',(1.,0.,0.));
#15186=DIRECTION('center_axis',(0.,0.,-1.));
#15187=DIRECTION('ref_axis',(1.,0.,0.));
#15188=DIRECTION('center_axis',(0.,0.,-1.));
#15189=DIRECTION('ref_axis',(1.,0.,0.));
#15190=DIRECTION('center_axis',(0.,0.,-1.));
#15191=DIRECTION('ref_axis',(1.,0.,0.));
#15192=DIRECTION('center_axis',(0.,0.,-1.));
#15193=DIRECTION('ref_axis',(1.,0.,0.));
#15194=DIRECTION('center_axis',(0.,0.,-1.));
#15195=DIRECTION('ref_axis',(1.,0.,0.));
#15196=DIRECTION('center_axis',(0.,0.,-1.));
#15197=DIRECTION('ref_axis',(1.,0.,0.));
#15198=DIRECTION('center_axis',(0.,0.,-1.));
#15199=DIRECTION('ref_axis',(1.,0.,0.));
#15200=DIRECTION('center_axis',(0.,0.,-1.));
#15201=DIRECTION('ref_axis',(1.,0.,0.));
#15202=DIRECTION('center_axis',(0.,0.,1.));
#15203=DIRECTION('ref_axis',(1.,0.,0.));
#15204=DIRECTION('center_axis',(0.,0.,-1.));
#15205=DIRECTION('ref_axis',(1.,0.,0.));
#15206=DIRECTION('',(0.,0.,-1.));
#15207=DIRECTION('center_axis',(0.,0.,1.));
#15208=DIRECTION('ref_axis',(1.,0.,0.));
#15209=DIRECTION('center_axis',(0.,0.,-1.));
#15210=DIRECTION('ref_axis',(1.,0.,0.));
#15211=DIRECTION('',(0.,0.,-1.));
#15212=DIRECTION('center_axis',(0.,0.,1.));
#15213=DIRECTION('ref_axis',(1.,0.,0.));
#15214=DIRECTION('center_axis',(0.,0.,-1.));
#15215=DIRECTION('ref_axis',(1.,0.,0.));
#15216=DIRECTION('',(0.,0.,-1.));
#15217=DIRECTION('center_axis',(0.,0.,1.));
#15218=DIRECTION('ref_axis',(1.,0.,0.));
#15219=DIRECTION('center_axis',(0.,0.,-1.));
#15220=DIRECTION('ref_axis',(1.,0.,0.));
#15221=DIRECTION('',(0.,0.,-1.));
#15222=DIRECTION('center_axis',(0.,0.,1.));
#15223=DIRECTION('ref_axis',(1.,0.,0.));
#15224=DIRECTION('center_axis',(0.,0.,-1.));
#15225=DIRECTION('ref_axis',(1.,0.,0.));
#15226=DIRECTION('',(0.,0.,-1.));
#15227=DIRECTION('center_axis',(0.,0.,1.));
#15228=DIRECTION('ref_axis',(1.,0.,0.));
#15229=DIRECTION('center_axis',(0.,0.,-1.));
#15230=DIRECTION('ref_axis',(1.,0.,0.));
#15231=DIRECTION('',(0.,0.,-1.));
#15232=DIRECTION('center_axis',(0.,0.,1.));
#15233=DIRECTION('ref_axis',(1.,0.,0.));
#15234=DIRECTION('center_axis',(0.,0.,-1.));
#15235=DIRECTION('ref_axis',(1.,0.,0.));
#15236=DIRECTION('',(0.,0.,-1.));
#15237=DIRECTION('center_axis',(0.,0.,1.));
#15238=DIRECTION('ref_axis',(1.,0.,0.));
#15239=DIRECTION('center_axis',(0.,0.,-1.));
#15240=DIRECTION('ref_axis',(1.,0.,0.));
#15241=DIRECTION('',(0.,0.,-1.));
#15242=DIRECTION('center_axis',(0.,0.,1.));
#15243=DIRECTION('ref_axis',(1.,0.,0.));
#15244=DIRECTION('center_axis',(0.,0.,-1.));
#15245=DIRECTION('ref_axis',(1.,0.,0.));
#15246=DIRECTION('',(0.,0.,-1.));
#15247=DIRECTION('center_axis',(0.,0.,1.));
#15248=DIRECTION('ref_axis',(1.,0.,0.));
#15249=DIRECTION('center_axis',(0.,0.,-1.));
#15250=DIRECTION('ref_axis',(1.,0.,0.));
#15251=DIRECTION('',(0.,0.,-1.));
#15252=DIRECTION('center_axis',(0.,0.,1.));
#15253=DIRECTION('ref_axis',(1.,0.,0.));
#15254=DIRECTION('center_axis',(0.,0.,-1.));
#15255=DIRECTION('ref_axis',(1.,0.,0.));
#15256=DIRECTION('',(0.,0.,-1.));
#15257=DIRECTION('center_axis',(-0.707106781186549,0.707106781186546,0.));
#15258=DIRECTION('ref_axis',(-0.707106781186546,-0.707106781186549,0.));
#15259=DIRECTION('',(0.,0.,1.));
#15260=DIRECTION('',(-0.707106781186546,-0.707106781186549,0.));
#15261=DIRECTION('',(0.,0.,1.));
#15262=DIRECTION('center_axis',(0.707106781186549,0.707106781186546,0.));
#15263=DIRECTION('ref_axis',(-0.707106781186546,0.707106781186549,0.));
#15264=DIRECTION('',(0.,0.,1.));
#15265=DIRECTION('',(-0.707106781186546,0.707106781186549,0.));
#15266=DIRECTION('',(0.,0.,1.));
#15267=DIRECTION('center_axis',(0.707106781186549,-0.707106781186546,0.));
#15268=DIRECTION('ref_axis',(0.707106781186546,0.707106781186549,0.));
#15269=DIRECTION('',(0.707106781186546,0.707106781186549,0.));
#15270=DIRECTION('',(0.,0.,1.));
#15271=DIRECTION('center_axis',(0.,-1.,0.));
#15272=DIRECTION('ref_axis',(1.,0.,0.));
#15273=DIRECTION('',(1.,0.,0.));
#15274=DIRECTION('',(0.,0.,1.));
#15275=DIRECTION('center_axis',(-0.707106781186549,-0.707106781186546,0.));
#15276=DIRECTION('ref_axis',(0.707106781186546,-0.707106781186549,0.));
#15277=DIRECTION('',(0.707106781186546,-0.707106781186549,0.));
#15278=DIRECTION('center_axis',(0.,0.,1.));
#15279=DIRECTION('ref_axis',(1.,0.,0.));
#15280=DIRECTION('',(1.,0.,0.));
#15281=DIRECTION('',(0.,-1.,0.));
#15282=DIRECTION('',(0.,1.,0.));
#15283=DIRECTION('center_axis',(0.,1.,0.));
#15284=DIRECTION('ref_axis',(1.,0.,0.));
#15285=DIRECTION('',(0.,0.,-1.));
#15286=DIRECTION('',(0.,0.,-1.));
#15287=DIRECTION('',(1.,0.,0.));
#15288=DIRECTION('center_axis',(0.,-1.,0.));
#15289=DIRECTION('ref_axis',(-1.,0.,0.));
#15290=DIRECTION('',(0.,0.,-1.));
#15291=DIRECTION('',(0.,0.,-1.));
#15292=DIRECTION('center_axis',(-1.,0.,0.));
#15293=DIRECTION('ref_axis',(0.,1.,0.));
#15294=DIRECTION('',(0.,1.,0.));
#15295=DIRECTION('',(0.,0.,-1.));
#15296=DIRECTION('center_axis',(0.,-1.,0.));
#15297=DIRECTION('ref_axis',(-1.,0.,0.));
#15298=DIRECTION('',(-1.,0.,0.));
#15299=DIRECTION('',(0.,0.,-1.));
#15300=DIRECTION('center_axis',(1.,0.,0.));
#15301=DIRECTION('ref_axis',(0.,-1.,0.));
#15302=DIRECTION('',(0.,-1.,0.));
#15303=DIRECTION('center_axis',(0.,0.,-1.));
#15304=DIRECTION('ref_axis',(-1.,0.,0.));
#18160=CARTESIAN_POINT('',(0.,0.,0.));
#18161=CARTESIAN_POINT('Origin',(363.987734179926,50.,25.7372649179816));
#18162=CARTESIAN_POINT('',(362.487734179926,50.,25.7372649179816));
#18163=CARTESIAN_POINT('Origin',(363.987734179926,50.,25.7372649179816));
#18164=CARTESIAN_POINT('',(362.487734179926,53.,25.7372649179816));
#18165=CARTESIAN_POINT('',(362.487734179926,50.,25.7372649179816));
#18166=CARTESIAN_POINT('Origin',(363.987734179926,53.,25.7372649179816));
#18167=CARTESIAN_POINT('Origin',(368.021785697154,53.,3.89451831659521));
#18168=CARTESIAN_POINT('',(370.021785697154,53.,3.89451831659521));
#18169=CARTESIAN_POINT('Origin',(368.021785697154,53.,3.89451831659521));
#18170=CARTESIAN_POINT('',(370.021785697154,50.,3.89451831659521));
#18171=CARTESIAN_POINT('',(370.021785697154,53.,3.89451831659521));
#18172=CARTESIAN_POINT('Origin',(368.021785697154,50.,3.89451831659521));
#18173=CARTESIAN_POINT('Origin',(360.021785697154,53.,3.89451831659521));
#18174=CARTESIAN_POINT('',(362.021785697154,53.,3.89451831659521));
#18175=CARTESIAN_POINT('Origin',(360.021785697154,53.,3.89451831659521));
#18176=CARTESIAN_POINT('',(362.021785697154,50.,3.89451831659521));
#18177=CARTESIAN_POINT('',(362.021785697154,53.,3.89451831659521));
#18178=CARTESIAN_POINT('Origin',(360.021785697154,50.,3.89451831659521));
#18179=CARTESIAN_POINT('Origin',(367.952200273994,48.,28.4747649179816));
#18180=CARTESIAN_POINT('',(371.916666368061,50.,28.4747649179816));
#18181=CARTESIAN_POINT('',(371.916666368061,48.,30.4747649179816));
#18182=CARTESIAN_POINT('Origin',(371.916666368061,48.,28.4747649179816));
#18183=CARTESIAN_POINT('',(356.058801991792,48.,30.4747649179816));
#18184=CARTESIAN_POINT('',(367.952200273994,48.,30.4747649179816));
#18185=CARTESIAN_POINT('',(356.058801991792,50.,28.4747649179816));
#18186=CARTESIAN_POINT('Origin',(356.058801991792,48.,28.4747649179816));
#18187=CARTESIAN_POINT('',(367.952200273994,50.,28.4747649179816));
#18188=CARTESIAN_POINT('Origin',(363.987734179926,35.4644660940673,30.4747649179816));
#18189=CARTESIAN_POINT('',(371.916666368061,32.0710678118655,30.4747649179816));
#18190=CARTESIAN_POINT('',(371.916666368061,50.,30.4747649179816));
#18191=CARTESIAN_POINT('',(378.987734179926,25.,30.4747649179816));
#18192=CARTESIAN_POINT('',(378.987734179926,25.,30.4747649179816));
#18193=CARTESIAN_POINT('',(371.916666368061,17.9289321881345,30.4747649179816));
#18194=CARTESIAN_POINT('',(378.987734179926,25.,30.4747649179816));
#18195=CARTESIAN_POINT('',(356.058801991792,17.9289321881345,30.4747649179816));
#18196=CARTESIAN_POINT('',(371.916666368061,17.9289321881345,30.4747649179816));
#18197=CARTESIAN_POINT('',(348.987734179926,25.,30.4747649179816));
#18198=CARTESIAN_POINT('',(348.987734179926,25.,30.4747649179816));
#18199=CARTESIAN_POINT('',(356.058801991792,32.0710678118655,30.4747649179816));
#18200=CARTESIAN_POINT('',(348.987734179926,25.,30.4747649179816));
#18201=CARTESIAN_POINT('',(356.058801991792,50.,30.4747649179816));
#18202=CARTESIAN_POINT('',(362.381415464215,29.,30.4747649179816));
#18203=CARTESIAN_POINT('Origin',(363.881415464215,29.,30.4747649179816));
#18204=CARTESIAN_POINT('',(353.131415464215,25.,30.4747649179816));
#18205=CARTESIAN_POINT('Origin',(354.631415464215,25.,30.4747649179816));
#18206=CARTESIAN_POINT('',(367.006415464215,21.,30.4747649179816));
#18207=CARTESIAN_POINT('Origin',(368.506415464215,21.,30.4747649179816));
#18208=CARTESIAN_POINT('',(357.756415464215,21.,30.4747649179816));
#18209=CARTESIAN_POINT('Origin',(359.256415464215,21.,30.4747649179816));
#18210=CARTESIAN_POINT('',(362.381415464215,25.,30.4747649179816));
#18211=CARTESIAN_POINT('Origin',(363.881415464215,25.,30.4747649179816));
#18212=CARTESIAN_POINT('',(362.381415464215,21.,30.4747649179816));
#18213=CARTESIAN_POINT('Origin',(363.881415464215,21.,30.4747649179816));
#18214=CARTESIAN_POINT('',(367.006415464215,25.,30.4747649179816));
#18215=CARTESIAN_POINT('Origin',(368.506415464215,25.,30.4747649179816));
#18216=CARTESIAN_POINT('',(357.756415464215,25.,30.4747649179816));
#18217=CARTESIAN_POINT('Origin',(359.256415464215,25.,30.4747649179816));
#18218=CARTESIAN_POINT('',(357.756415464215,29.,30.4747649179816));
#18219=CARTESIAN_POINT('Origin',(359.256415464215,29.,30.4747649179816));
#18220=CARTESIAN_POINT('',(367.006415464215,29.,30.4747649179816));
#18221=CARTESIAN_POINT('Origin',(368.506415464215,29.,30.4747649179816));
#18222=CARTESIAN_POINT('',(371.631415464215,25.,30.4747649179816));
#18223=CARTESIAN_POINT('Origin',(373.131415464215,25.,30.4747649179816));
#18224=CARTESIAN_POINT('Origin',(356.058801991792,49.0313730334031,29.9747649179816));
#18225=CARTESIAN_POINT('',(356.058801991792,53.,30.4747649179816));
#18226=CARTESIAN_POINT('',(356.058801991792,49.0313730334031,33.9747649179816));
#18227=CARTESIAN_POINT('Origin',(356.058801991792,49.0313730334031,29.9747649179816));
#18228=CARTESIAN_POINT('',(371.916666368061,49.0313730334031,33.9747649179816));
#18229=CARTESIAN_POINT('',(356.058801991792,49.0313730334031,33.9747649179816));
#18230=CARTESIAN_POINT('',(371.916666368061,53.,30.4747649179816));
#18231=CARTESIAN_POINT('Origin',(371.916666368061,49.0313730334031,29.9747649179816));
#18232=CARTESIAN_POINT('',(356.058801991792,53.,30.4747649179816));
#18233=CARTESIAN_POINT('Origin',(363.987734179926,35.4644660940673,33.9747649179816));
#18234=CARTESIAN_POINT('',(356.058801991792,32.0710678118655,33.9747649179816));
#18235=CARTESIAN_POINT('',(356.058801991792,50.,33.9747649179816));
#18236=CARTESIAN_POINT('',(348.987734179926,25.,33.9747649179816));
#18237=CARTESIAN_POINT('',(348.987734179926,25.,33.9747649179816));
#18238=CARTESIAN_POINT('',(356.058801991792,17.9289321881345,33.9747649179816));
#18239=CARTESIAN_POINT('',(348.987734179926,25.,33.9747649179816));
#18240=CARTESIAN_POINT('',(371.916666368061,17.9289321881345,33.9747649179816));
#18241=CARTESIAN_POINT('',(371.916666368061,17.9289321881345,33.9747649179816));
#18242=CARTESIAN_POINT('',(378.987734179926,25.,33.9747649179816));
#18243=CARTESIAN_POINT('',(378.987734179926,25.,33.9747649179816));
#18244=CARTESIAN_POINT('',(371.916666368061,32.0710678118655,33.9747649179816));
#18245=CARTESIAN_POINT('',(378.987734179926,25.,33.9747649179816));
#18246=CARTESIAN_POINT('',(371.916666368061,50.,33.9747649179816));
#18247=CARTESIAN_POINT('',(371.631415464215,25.,33.9747649179816));
#18248=CARTESIAN_POINT('Origin',(373.131415464215,25.,33.9747649179816));
#18249=CARTESIAN_POINT('',(367.006415464215,29.,33.9747649179816));
#18250=CARTESIAN_POINT('Origin',(368.506415464215,29.,33.9747649179816));
#18251=CARTESIAN_POINT('',(357.756415464215,29.,33.9747649179816));
#18252=CARTESIAN_POINT('Origin',(359.256415464215,29.,33.9747649179816));
#18253=CARTESIAN_POINT('',(357.756415464215,25.,33.9747649179816));
#18254=CARTESIAN_POINT('Origin',(359.256415464215,25.,33.9747649179816));
#18255=CARTESIAN_POINT('',(367.006415464215,25.,33.9747649179816));
#18256=CARTESIAN_POINT('Origin',(368.506415464215,25.,33.9747649179816));
#18257=CARTESIAN_POINT('',(362.381415464215,21.,33.9747649179816));
#18258=CARTESIAN_POINT('Origin',(363.881415464215,21.,33.9747649179816));
#18259=CARTESIAN_POINT('',(362.381415464215,25.,33.9747649179816));
#18260=CARTESIAN_POINT('Origin',(363.881415464215,25.,33.9747649179816));
#18261=CARTESIAN_POINT('',(357.756415464215,21.,33.9747649179816));
#18262=CARTESIAN_POINT('Origin',(359.256415464215,21.,33.9747649179816));
#18263=CARTESIAN_POINT('',(367.006415464215,21.,33.9747649179816));
#18264=CARTESIAN_POINT('Origin',(368.506415464215,21.,33.9747649179816));
#18265=CARTESIAN_POINT('',(353.131415464215,25.,33.9747649179816));
#18266=CARTESIAN_POINT('Origin',(354.631415464215,25.,33.9747649179816));
#18267=CARTESIAN_POINT('',(362.381415464215,29.,33.9747649179816));
#18268=CARTESIAN_POINT('Origin',(363.881415464215,29.,33.9747649179816));
#18269=CARTESIAN_POINT('Origin',(373.131415464215,25.,30.4747649179816));
#18270=CARTESIAN_POINT('',(371.631415464215,25.,30.4747649179816));
#18271=CARTESIAN_POINT('Origin',(368.506415464215,29.,30.4747649179816));
#18272=CARTESIAN_POINT('',(367.006415464215,29.,30.4747649179816));
#18273=CARTESIAN_POINT('Origin',(359.256415464215,29.,30.4747649179816));
#18274=CARTESIAN_POINT('',(357.756415464215,29.,30.4747649179816));
#18275=CARTESIAN_POINT('Origin',(359.256415464215,25.,30.4747649179816));
#18276=CARTESIAN_POINT('',(357.756415464215,25.,30.4747649179816));
#18277=CARTESIAN_POINT('Origin',(368.506415464215,25.,30.4747649179816));
#18278=CARTESIAN_POINT('',(367.006415464215,25.,30.4747649179816));
#18279=CARTESIAN_POINT('Origin',(363.881415464215,21.,30.4747649179816));
#18280=CARTESIAN_POINT('',(362.381415464215,21.,30.4747649179816));
#18281=CARTESIAN_POINT('Origin',(363.881415464215,25.,30.4747649179816));
#18282=CARTESIAN_POINT('',(362.381415464215,25.,30.4747649179816));
#18283=CARTESIAN_POINT('Origin',(359.256415464215,21.,30.4747649179816));
#18284=CARTESIAN_POINT('',(357.756415464215,21.,30.4747649179816));
#18285=CARTESIAN_POINT('Origin',(368.506415464215,21.,30.4747649179816));
#18286=CARTESIAN_POINT('',(367.006415464215,21.,30.4747649179816));
#18287=CARTESIAN_POINT('Origin',(354.631415464215,25.,30.4747649179816));
#18288=CARTESIAN_POINT('',(353.131415464215,25.,30.4747649179816));
#18289=CARTESIAN_POINT('Origin',(363.881415464215,29.,30.4747649179816));
#18290=CARTESIAN_POINT('',(362.381415464215,29.,30.4747649179816));
#18291=CARTESIAN_POINT('Origin',(356.058801991792,32.0710678118655,30.4747649179816));
#18292=CARTESIAN_POINT('',(348.987734179926,25.,30.4747649179816));
#18293=CARTESIAN_POINT('',(356.058801991792,32.0710678118655,30.4747649179816));
#18294=CARTESIAN_POINT('Origin',(378.987734179926,25.,30.4747649179816));
#18295=CARTESIAN_POINT('',(371.916666368061,32.0710678118655,30.4747649179816));
#18296=CARTESIAN_POINT('',(378.987734179926,25.,30.4747649179816));
#18297=CARTESIAN_POINT('Origin',(371.916666368061,17.9289321881345,30.4747649179816));
#18298=CARTESIAN_POINT('',(371.916666368061,17.9289321881345,30.4747649179816));
#18299=CARTESIAN_POINT('Origin',(356.058801991792,17.9289321881345,30.4747649179816));
#18300=CARTESIAN_POINT('',(356.058801991792,17.9289321881345,30.4747649179816));
#18301=CARTESIAN_POINT('Origin',(348.987734179926,25.,30.4747649179816));
#18302=CARTESIAN_POINT('Origin',(363.987734179926,35.4644660940673,19.4747649179816));
#18303=CARTESIAN_POINT('',(371.916666368061,50.,19.4747649179816));
#18304=CARTESIAN_POINT('',(356.058801991792,50.,19.4747649179816));
#18305=CARTESIAN_POINT('',(367.952200273994,50.,19.4747649179816));
#18306=CARTESIAN_POINT('',(371.916666368061,32.0710678118655,19.4747649179816));
#18307=CARTESIAN_POINT('',(371.916666368061,50.,19.4747649179816));
#18308=CARTESIAN_POINT('',(378.987734179926,25.,19.4747649179816));
#18309=CARTESIAN_POINT('',(378.987734179926,25.,19.4747649179816));
#18310=CARTESIAN_POINT('',(371.916666368061,17.9289321881345,19.4747649179816));
#18311=CARTESIAN_POINT('',(378.987734179926,25.,19.4747649179816));
#18312=CARTESIAN_POINT('',(356.058801991792,17.9289321881345,19.4747649179816));
#18313=CARTESIAN_POINT('',(371.916666368061,17.9289321881345,19.4747649179816));
#18314=CARTESIAN_POINT('',(348.987734179926,25.,19.4747649179816));
#18315=CARTESIAN_POINT('',(348.987734179926,25.,19.4747649179816));
#18316=CARTESIAN_POINT('',(356.058801991792,32.0710678118655,19.4747649179816));
#18317=CARTESIAN_POINT('',(348.987734179926,25.,19.4747649179816));
#18318=CARTESIAN_POINT('',(356.058801991792,50.,19.4747649179816));
#18319=CARTESIAN_POINT('',(371.631415464215,25.,19.4747649179816));
#18320=CARTESIAN_POINT('Origin',(373.131415464215,25.,19.4747649179816));
#18321=CARTESIAN_POINT('',(367.006415464215,29.,19.4747649179816));
#18322=CARTESIAN_POINT('Origin',(368.506415464215,29.,19.4747649179816));
#18323=CARTESIAN_POINT('',(357.756415464215,29.,19.4747649179816));
#18324=CARTESIAN_POINT('Origin',(359.256415464215,29.,19.4747649179816));
#18325=CARTESIAN_POINT('',(357.756415464215,25.,19.4747649179816));
#18326=CARTESIAN_POINT('Origin',(359.256415464215,25.,19.4747649179816));
#18327=CARTESIAN_POINT('',(367.006415464215,25.,19.4747649179816));
#18328=CARTESIAN_POINT('Origin',(368.506415464215,25.,19.4747649179816));
#18329=CARTESIAN_POINT('',(362.381415464215,21.,19.4747649179816));
#18330=CARTESIAN_POINT('Origin',(363.881415464215,21.,19.4747649179816));
#18331=CARTESIAN_POINT('',(362.381415464215,25.,19.4747649179816));
#18332=CARTESIAN_POINT('Origin',(363.881415464215,25.,19.4747649179816));
#18333=CARTESIAN_POINT('',(357.756415464215,21.,19.4747649179816));
#18334=CARTESIAN_POINT('Origin',(359.256415464215,21.,19.4747649179816));
#18335=CARTESIAN_POINT('',(367.006415464215,21.,19.4747649179816));
#18336=CARTESIAN_POINT('Origin',(368.506415464215,21.,19.4747649179816));
#18337=CARTESIAN_POINT('',(353.131415464215,25.,19.4747649179816));
#18338=CARTESIAN_POINT('Origin',(354.631415464215,25.,19.4747649179816));
#18339=CARTESIAN_POINT('',(362.381415464215,29.,19.4747649179816));
#18340=CARTESIAN_POINT('Origin',(363.881415464215,29.,19.4747649179816));
#18341=CARTESIAN_POINT('Origin',(373.131415464215,25.,19.4747649179816));
#18342=CARTESIAN_POINT('',(371.631415464215,25.,22.9997649179816));
#18343=CARTESIAN_POINT('Origin',(373.131415464215,25.,22.9997649179816));
#18344=CARTESIAN_POINT('',(371.631415464215,25.,19.4747649179816));
#18345=CARTESIAN_POINT('Origin',(368.506415464215,29.,19.4747649179816));
#18346=CARTESIAN_POINT('',(367.006415464215,29.,22.9997649179816));
#18347=CARTESIAN_POINT('Origin',(368.506415464215,29.,22.9997649179816));
#18348=CARTESIAN_POINT('',(367.006415464215,29.,19.4747649179816));
#18349=CARTESIAN_POINT('Origin',(359.256415464215,29.,19.4747649179816));
#18350=CARTESIAN_POINT('',(357.756415464215,29.,22.9997649179816));
#18351=CARTESIAN_POINT('Origin',(359.256415464215,29.,22.9997649179816));
#18352=CARTESIAN_POINT('',(357.756415464215,29.,19.4747649179816));
#18353=CARTESIAN_POINT('Origin',(359.256415464215,25.,19.4747649179816));
#18354=CARTESIAN_POINT('',(357.756415464215,25.,22.9997649179816));
#18355=CARTESIAN_POINT('Origin',(359.256415464215,25.,22.9997649179816));
#18356=CARTESIAN_POINT('',(357.756415464215,25.,19.4747649179816));
#18357=CARTESIAN_POINT('Origin',(368.506415464215,25.,19.4747649179816));
#18358=CARTESIAN_POINT('',(367.006415464215,25.,22.9997649179816));
#18359=CARTESIAN_POINT('Origin',(368.506415464215,25.,22.9997649179816));
#18360=CARTESIAN_POINT('',(367.006415464215,25.,19.4747649179816));
#18361=CARTESIAN_POINT('Origin',(363.881415464215,21.,19.4747649179816));
#18362=CARTESIAN_POINT('',(362.381415464215,21.,22.9997649179816));
#18363=CARTESIAN_POINT('Origin',(363.881415464215,21.,22.9997649179816));
#18364=CARTESIAN_POINT('',(362.381415464215,21.,19.4747649179816));
#18365=CARTESIAN_POINT('Origin',(363.881415464215,25.,19.4747649179816));
#18366=CARTESIAN_POINT('',(362.381415464215,25.,22.9997649179816));
#18367=CARTESIAN_POINT('Origin',(363.881415464215,25.,22.9997649179816));
#18368=CARTESIAN_POINT('',(362.381415464215,25.,19.4747649179816));
#18369=CARTESIAN_POINT('Origin',(359.256415464215,21.,19.4747649179816));
#18370=CARTESIAN_POINT('',(357.756415464215,21.,22.9997649179816));
#18371=CARTESIAN_POINT('Origin',(359.256415464215,21.,22.9997649179816));
#18372=CARTESIAN_POINT('',(357.756415464215,21.,19.4747649179816));
#18373=CARTESIAN_POINT('Origin',(368.506415464215,21.,19.4747649179816));
#18374=CARTESIAN_POINT('',(367.006415464215,21.,22.9997649179816));
#18375=CARTESIAN_POINT('Origin',(368.506415464215,21.,22.9997649179816));
#18376=CARTESIAN_POINT('',(367.006415464215,21.,19.4747649179816));
#18377=CARTESIAN_POINT('Origin',(354.631415464215,25.,19.4747649179816));
#18378=CARTESIAN_POINT('',(353.131415464215,25.,22.9997649179816));
#18379=CARTESIAN_POINT('Origin',(354.631415464215,25.,22.9997649179816));
#18380=CARTESIAN_POINT('',(353.131415464215,25.,19.4747649179816));
#18381=CARTESIAN_POINT('Origin',(363.881415464215,29.,19.4747649179816));
#18382=CARTESIAN_POINT('',(362.381415464215,29.,22.9997649179816));
#18383=CARTESIAN_POINT('Origin',(363.881415464215,29.,22.9997649179816));
#18384=CARTESIAN_POINT('',(362.381415464215,29.,19.4747649179816));
#18385=CARTESIAN_POINT('Origin',(356.058801991792,32.0710678118655,19.4747649179816));
#18386=CARTESIAN_POINT('',(348.987734179926,25.,22.9997649179816));
#18387=CARTESIAN_POINT('',(348.987734179926,25.,19.4747649179816));
#18388=CARTESIAN_POINT('',(356.058801991792,32.0710678118655,22.9997649179816));
#18389=CARTESIAN_POINT('',(358.889384609376,34.9016504294496,22.9997649179816));
#18390=CARTESIAN_POINT('',(356.058801991792,32.0710678118655,19.4747649179816));
#18391=CARTESIAN_POINT('Origin',(378.987734179926,25.,19.4747649179816));
#18392=CARTESIAN_POINT('',(371.916666368061,32.0710678118655,22.9997649179816));
#18393=CARTESIAN_POINT('',(371.916666368061,32.0710678118655,19.4747649179816));
#18394=CARTESIAN_POINT('',(378.987734179926,25.,22.9997649179816));
#18395=CARTESIAN_POINT('',(372.62161765641,31.3661165235168,22.9997649179816));
#18396=CARTESIAN_POINT('',(378.987734179926,25.,19.4747649179816));
#18397=CARTESIAN_POINT('Origin',(371.916666368061,17.9289321881345,19.4747649179816));
#18398=CARTESIAN_POINT('',(371.916666368061,17.9289321881345,22.9997649179816));
#18399=CARTESIAN_POINT('',(374.31831679751,20.3305826175841,22.9997649179816));
#18400=CARTESIAN_POINT('',(371.916666368061,17.9289321881345,19.4747649179816));
#18401=CARTESIAN_POINT('Origin',(356.058801991792,17.9289321881345,19.4747649179816));
#18402=CARTESIAN_POINT('',(356.058801991792,17.9289321881345,22.9997649179816));
#18403=CARTESIAN_POINT('',(360.023268085859,17.9289321881345,22.9997649179816));
#18404=CARTESIAN_POINT('',(356.058801991792,17.9289321881345,19.4747649179816));
#18405=CARTESIAN_POINT('Origin',(348.987734179926,25.,19.4747649179816));
#18406=CARTESIAN_POINT('',(350.12161765641,23.8661165235168,22.9997649179816));
#18407=CARTESIAN_POINT('Origin',(363.987734179926,35.4644660940673,22.9997649179816));
#18408=CARTESIAN_POINT('',(356.058801991792,50.,22.9997649179816));
#18409=CARTESIAN_POINT('',(371.916666368061,50.,22.9997649179816));
#18410=CARTESIAN_POINT('',(367.952200273994,50.,22.9997649179816));
#18411=CARTESIAN_POINT('',(356.058801991792,44.2322330470336,22.9997649179816));
#18412=CARTESIAN_POINT('',(371.916666368061,33.7677669529664,22.9997649179816));
#18413=CARTESIAN_POINT('Origin',(356.058801991792,53.,30.4747649179816));
#18414=CARTESIAN_POINT('',(356.058801991792,53.,-0.000235082018433808));
#18415=CARTESIAN_POINT('',(356.058801991792,53.,30.4747649179816));
#18416=CARTESIAN_POINT('',(371.916666368061,53.,-0.000235082018433808));
#18417=CARTESIAN_POINT('',(371.916666368061,53.,30.4747649179816));
#18418=CARTESIAN_POINT('',(356.058801991792,53.,-0.000235082018433808));
#18419=CARTESIAN_POINT('Origin',(371.916666368061,50.,30.4747649179816));
#18420=CARTESIAN_POINT('',(356.058801991792,50.,30.4747649179816));
#18421=CARTESIAN_POINT('',(371.916666368061,50.,30.4747649179816));
#18422=CARTESIAN_POINT('Origin',(356.058801991792,50.,30.4747649179816));
#18423=CARTESIAN_POINT('',(356.058801991792,50.,-0.000235082018433808));
#18424=CARTESIAN_POINT('',(356.058801991792,50.,-0.000235082018433808));
#18425=CARTESIAN_POINT('',(356.058801991792,50.,30.4747649179816));
#18426=CARTESIAN_POINT('Origin',(371.916666368061,50.,30.4747649179816));
#18427=CARTESIAN_POINT('',(371.916666368061,50.,-0.000235082018433808));
#18428=CARTESIAN_POINT('',(371.916666368061,50.,-0.000235082018433808));
#18429=CARTESIAN_POINT('',(371.916666368061,50.,30.4747649179816));
#18430=CARTESIAN_POINT('Origin',(371.916666368061,53.,30.4747649179816));
#18431=CARTESIAN_POINT('',(371.916666368061,53.,-0.000235082018433808));
#18432=CARTESIAN_POINT('Origin',(363.987734179926,51.5,-0.000235082018433808));
#19196=UNCERTAINTY_MEASURE_WITH_UNIT(LENGTH_MEASURE(0.01),#19221,
'DISTANCE_ACCURACY_VALUE',
'Maximum model space distance between geometric entities at asserted c
onnectivities');
#19204=UNCERTAINTY_MEASURE_WITH_UNIT(LENGTH_MEASURE(0.01),#19221,
'DISTANCE_ACCURACY_VALUE',
'Maximum model space distance between geometric entities at asserted c
onnectivities');
#19212=(
GEOMETRIC_REPRESENTATION_CONTEXT(3)
GLOBAL_UNCERTAINTY_ASSIGNED_CONTEXT((#19196))
GLOBAL_UNIT_ASSIGNED_CONTEXT((#19221,#19223,#19224))
REPRESENTATION_CONTEXT('','3D')
);
#19220=(
GEOMETRIC_REPRESENTATION_CONTEXT(3)
GLOBAL_UNCERTAINTY_ASSIGNED_CONTEXT((#19204))
GLOBAL_UNIT_ASSIGNED_CONTEXT((#19221,#19223,#19224))
REPRESENTATION_CONTEXT('','3D')
);
#19221=(
LENGTH_UNIT()
NAMED_UNIT(*)
SI_UNIT(.MILLI.,.METRE.)
);
#19223=(
NAMED_UNIT(*)
PLANE_ANGLE_UNIT()
SI_UNIT($,.RADIAN.)
);
#19224=(
NAMED_UNIT(*)
SI_UNIT($,.STERADIAN.)
SOLID_ANGLE_UNIT()
);
#19232=SHAPE_DEFINITION_REPRESENTATION(#19247,#19276);
#19247=PRODUCT_DEFINITION_SHAPE('',$,#19292);
#19276=SHAPE_REPRESENTATION('',(#12374),#19212);
#19284=PRODUCT_DEFINITION_CONTEXT('part definition',#19331,'design');
#19292=PRODUCT_DEFINITION('Bracket_01 (1)','Bracket_01 (1)',#19307,#19284);
#19307=PRODUCT_DEFINITION_FORMATION('',$,#19340);
#19331=APPLICATION_CONTEXT(
'Core Data for Automotive Mechanical Design Process');
#19332=PRODUCT_CONTEXT('part definition',#19331,'mechanical');
#19340=PRODUCT('Bracket_01 (1)','Bracket_01 (1)',$,(#19332));
#19376=COLOUR_RGB('Dark Blue',0.08,0.2,0.34);
#19377=FILL_AREA_STYLE_COLOUR('',#19376);
#19378=FILL_AREA_STYLE('',(#19377));
#19379=SURFACE_STYLE_FILL_AREA(#19378);
#19380=SURFACE_SIDE_STYLE('',(#19379));
#19381=SURFACE_STYLE_USAGE(.BOTH.,#19380);
#19382=PRESENTATION_STYLE_ASSIGNMENT((#19381));
ENDSEC;
END-ISO-10303-21;
